ISO-10303-21;
HEADER;
FILE_DESCRIPTION (('STEP AP214'),
    '1' );
FILE_NAME ('hex flange bolt small_iso_ISO 4162 - M6 x 25 x 25-C.step',
    '2026-09-24T10:26:00',
    ( '' ),
    ( '' ),
    'SwSTEP 2.0',
    'SolidWorks 2026',
    '' );
FILE_SCHEMA (( 'AUTOMOTIVE_DESIGN' ));
ENDSEC;

DATA;
#13=DIRECTION ( 'NONE',  ( 0.000000000000000000, 4.440892098500621231E-16, 1.000000000000000000 ) ) ;
#34=CONICAL_SURFACE ( 'NONE', #739, 4.000000000000004441, 1.047197551196600296 ) ;
#46=FILL_AREA_STYLE ('',( #8750 ) ) ;
#47=VERTEX_POINT ( 'NONE', #6364 ) ;
#48=AXIS2_PLACEMENT_3D ( 'NONE', #14299, #4291, #8725 ) ;
#58=EDGE_CURVE ( 'NONE', #2255, #14288, #3932, .T. ) ;
#70=LINE ( 'NONE', #7950, #11481 ) ;
#88=FACE_OUTER_BOUND ( 'NONE', #2247, .T. ) ;
#104=CARTESIAN_POINT ( 'NONE',  ( 4.942471129496375681, -1.621204395475712046, 4.000000000000003553 ) ) ;
#111=CARTESIAN_POINT ( 'NONE',  ( 5.551115123125782702E-14, 3.464101615137764156, 2.000000000000001776 ) ) ;
#133=DIRECTION ( 'NONE',  ( -1.000000000000000000, 2.551526159633733968E-19, 1.987661601597216239E-18 ) ) ;
#142=CARTESIAN_POINT ( 'NONE',  ( 5.085009042717538286, 2.271170964606955778, 4.066216496625539634 ) ) ;
#152=CARTESIAN_POINT ( 'NONE',  ( 6.800000000000028244, -4.618802153517003184, 0.000000000000000000 ) ) ;
#156=CARTESIAN_POINT ( 'NONE',  ( 0.2484800633749933707, -4.430380094434230642, -0.3263565795981031581 ) ) ;
#165=DIRECTION ( 'NONE',  ( 1.734723475976770502E-18, -4.440892098500621231E-16, -1.000000000000000000 ) ) ;
#167=CARTESIAN_POINT ( 'NONE',  ( 0.000000000000000000, 0.000000000000000000, 0.000000000000000000 ) ) ;
#171=PRODUCT_DEFINITION_SHAPE ( 'NONE', 'NONE',  #7761 ) ;
#183=ORIENTED_EDGE ( 'NONE', *, *, #4806, .T. ) ;
#196=AXIS2_PLACEMENT_3D ( 'NONE', #5459, #4385, #14329 ) ;
#208=AXIS2_PLACEMENT_3D ( 'NONE', #12173, #7777, #14450 ) ;
#216=CARTESIAN_POINT ( 'NONE',  ( 0.1391502195351374815, -4.241015250120806712, 0.6543461111163237920 ) ) ;
#244=B_SPLINE_CURVE_WITH_KNOTS ( 'NONE', 3,
 ( #6085, #473, #399, #10567, #328 ),
 .UNSPECIFIED., .F., .F.,
 ( 4, 1, 4 ),
 ( 0.000000000000000000, 0.002309401076758502321, 0.004618802153517004641 ),
 .UNSPECIFIED. ) ;
#249=DIRECTION ( 'NONE',  ( 1.000000000000000000, -2.551526159633733968E-19, -1.987661601597216239E-18 ) ) ;
#302=AXIS2_PLACEMENT_3D ( 'NONE', #9953, #7666, #5414 ) ;
#316=CARTESIAN_POINT ( 'NONE',  ( 5.000882498481321825, 2.309401076758504257, -4.000000000000005329 ) ) ;
#322=CARTESIAN_POINT ( 'NONE',  ( 4.960798468789974436, -4.316040323963732384, 0.6738506825564457570 ) ) ;
#328=CARTESIAN_POINT ( 'NONE',  ( 4.988724804725785944, -2.309401076758511806, -3.999999999999989786 ) ) ;
#338=ORIENTED_EDGE ( 'NONE', *, *, #3386, .T. ) ;
#346=CARTESIAN_POINT ( 'NONE',  ( 0.2484800633750008092, -2.497823135841239939, 3.673643420401929482 ) ) ;
#358=ORIENTED_EDGE ( 'NONE', *, *, #8649, .F. ) ;
#379=CARTESIAN_POINT ( 'NONE',  ( 4.851472949720997185, 2.694301256218259777, -3.333333333333333925 ) ) ;
#386=CARTESIAN_POINT ( 'NONE',  ( 5.076540720129295359, 2.330508241952946147, -4.036558682520523966 ) ) ;
#388=( BOUNDED_SURFACE ( )  B_SPLINE_SURFACE ( 3, 2, ( 
 ( #3636, #8070, #4659 ),
 ( #3858, #7047, #7120 ),
 ( #6973, #4862, #11444 ),
 ( #3572, #2599, #9324 ),
 ( #12766, #9250, #13809 ),
 ( #13596, #1568, #3776 ) ),
 .UNSPECIFIED., .F., .F., .T. ) 
 B_SPLINE_SURFACE_WITH_KNOTS ( ( 4, 2, 4 ),
 ( 3, 3 ),
 ( 0.01886032586153034776, 0.02121253401777977582, 0.02356474217402920734 ),
 ( 0.000000000000000000, 1.000000000000000000 ),
 .UNSPECIFIED. ) 
 GEOMETRIC_REPRESENTATION_ITEM ( )  RATIONAL_B_SPLINE_SURFACE ( (
 ( 1.000000000000000000, 0.8047781103519398016, 1.000000000000000000),
 ( 1.000000000000000000, 0.8123785825774555436, 1.000000000000000000),
 ( 1.000000000000000000, 0.8190671539561653614, 1.000000000000000000),
 ( 1.000000000000000000, 0.8192352255061488009, 1.000000000000000000),
 ( 1.000000000000000000, 0.8126129677041400434, 1.000000000000000000),
 ( 1.000000000000000000, 0.8047712537969720081, 1.000000000000000000) ) ) 
 REPRESENTATION_ITEM ( '' )  SURFACE ( )  );
#398=ORIENTED_EDGE ( 'NONE', *, *, #479, .T. ) ;
#399=CARTESIAN_POINT ( 'NONE',  ( 4.686019787951677174, -2.168404344971008868E-16, -4.000000000000015987 ) ) ;
#401=CARTESIAN_POINT ( 'NONE',  ( 6.800000000000028244, 1.327413925124860797E-15, 3.000000000000000000 ) ) ;
#404=FACE_OUTER_BOUND ( 'NONE', #14317, .T. ) ;
#416=CARTESIAN_POINT ( 'NONE',  ( 0.03421028094652689422, -3.072372537026350159, 2.678494666091049581 ) ) ;
#437=DIRECTION ( 'NONE',  ( 1.734723475976770502E-18, -4.440892098500621231E-16, -1.000000000000000000 ) ) ;
#451=B_SPLINE_CURVE_WITH_KNOTS ( 'NONE', 3,
 ( #1333, #11360, #8130, #1631, #322, #10560 ),
 .UNSPECIFIED., .F., .F.,
 ( 4, 2, 4 ),
 ( 0.000000000000000000, 0.002383230369971170957, 0.004766460739942341915 ),
 .UNSPECIFIED. ) ;
#459=ORIENTED_EDGE ( 'NONE', *, *, #3197, .T. ) ;
#465=EDGE_CURVE ( 'NONE', #9446, #7193, #8244, .T. ) ;
#473=CARTESIAN_POINT ( 'NONE',  ( 4.851472949720994521, 1.539600717839003430, -4.000000000000002665 ) ) ;
#479=EDGE_CURVE ( 'NONE', #8503, #4363, #3283, .T. ) ;
#492=ORIENTED_EDGE ( 'NONE', *, *, #7099, .T. ) ;
#515=CARTESIAN_POINT ( 'NONE',  ( 5.046772446839304926, -2.317775331972803610, -4.014504635506726871 ) ) ;
#522=EDGE_CURVE ( 'NONE', #47, #5931, #7516, .T. ) ;
#568=VERTEX_POINT ( 'NONE', #13389 ) ;
#571=EDGE_CURVE ( 'NONE', #8706, #2255, #3695, .T. ) ;
#593=CARTESIAN_POINT ( 'NONE',  ( 6.799999999999972289, -2.309401076758498039, -4.000000000000003553 ) ) ;
#627=CARTESIAN_POINT ( 'NONE',  ( 5.733169058567799681, -3.291357029458752715E-15, 6.438111078829122036 ) ) ;
#630=VERTEX_POINT ( 'NONE', #2390 ) ;
#638=CARTESIAN_POINT ( 'NONE',  ( 31.24550000000003536, -9.697272942312978198E-16, -3.000000000000000000 ) ) ;
#640=CARTESIAN_POINT ( 'NONE',  ( 5.056385618527004411, 4.642911450026675269, 0.000000000000000000 ) ) ;
#655=CARTESIAN_POINT ( 'NONE',  ( 5.733169058567799681, -3.291357029458752715E-15, 6.438111078829122036 ) ) ;
#672=CARTESIAN_POINT ( 'NONE',  ( 31.80000000000005045, 8.024914066595556114E-15, 2.445500000000030649 ) ) ;
#726=DIRECTION ( 'NONE',  ( 0.000000000000000000, 4.440892098500620738E-16, 1.000000000000000000 ) ) ;
#739=AXIS2_PLACEMENT_3D ( 'NONE', #9438, #3738, #8183 ) ;
#756=EDGE_CURVE ( 'NONE', #6205, #7193, #7281, .T. ) ;
#763=CARTESIAN_POINT ( 'NONE',  ( 0.000000000000000000, 2.081668171172168513E-14, 4.000000000000003553 ) ) ;
#770=ORIENTED_EDGE ( 'NONE', *, *, #14399, .F. ) ;
#787=AXIS2_PLACEMENT_3D ( 'NONE', #5564, #10033, #8932 ) ;
#805=CARTESIAN_POINT ( 'NONE',  ( 0.3572655899081733644, -4.618802153516988973, -1.387778780781445676E-14 ) ) ;
#832=DIRECTION ( 'NONE',  ( -1.000000000000000000, 2.551526159633733968E-19, 1.987661601597216239E-18 ) ) ;
#836=ORIENTED_EDGE ( 'NONE', *, *, #571, .T. ) ;
#838=EDGE_LOOP ( 'NONE', ( #5815, #338, #10885, #914 ) ) ;
#842=CARTESIAN_POINT ( 'NONE',  ( 5.035982117295204397, -2.314736229921469324, 4.009240756344432555 ) ) ;
#876=CARTESIAN_POINT ( 'NONE',  ( 5.005339752383233254, 2.263494164695158961, -4.079513104112302280 ) ) ;
#885=PRODUCT_DEFINITION_CONTEXT ( 'detailed design', #6041, 'design' ) ;
#889=CYLINDRICAL_SURFACE ( 'NONE', #48, 3.000000000000003553 ) ;
#910=CARTESIAN_POINT ( 'NONE',  ( 5.204170427930318053E-18, -9.648735898059816152E-16, -3.000000000000003553 ) ) ;
#914=ORIENTED_EDGE ( 'NONE', *, *, #2349, .F. ) ;
#926=CARTESIAN_POINT ( 'NONE',  ( 5.103531824934226080, -2.354098498486466351, -4.077418205400154427 ) ) ;
#947=CARTESIAN_POINT ( 'NONE',  ( 4.859329672868085481, 2.661112198169186982, -3.390818468129665586 ) ) ;
#951=ORIENTED_EDGE ( 'NONE', *, *, #8649, .T. ) ;
#966=FACE_OUTER_BOUND ( 'NONE', #2432, .T. ) ;
#968=( NAMED_UNIT ( * ) SI_UNIT ( $, .STERADIAN. ) SOLID_ANGLE_UNIT ( ) );
#1017=CARTESIAN_POINT ( 'NONE',  ( 4.851472949721049588, 4.233901974057263651, 0.6666666666666831720 ) ) ;
#1026=FACE_OUTER_BOUND ( 'NONE', #13706, .T. ) ;
#1057=EDGE_CURVE ( 'NONE', #8314, #47, #11892, .T. ) ;
#1109=ORIENTED_EDGE ( 'NONE', *, *, #11374, .T. ) ;
#1124=CIRCLE ( 'NONE', #11638, 4.000000000000004441 ) ;
#1140=SURFACE_SIDE_STYLE ('',( #10876 ) ) ;
#1157=CARTESIAN_POINT ( 'NONE',  ( 5.035982117295164429, -4.629472459842958187, -2.775691983046799710E-14 ) ) ;
#1164=DIRECTION ( 'NONE',  ( 1.000000000000000000, -2.551526159633733968E-19, -1.987661601597216239E-18 ) ) ;
#1165=DIRECTION ( 'NONE',  ( 1.000000000000000000, -2.551526159633733968E-19, -1.987661601597216239E-18 ) ) ;
#1172=PLANE ( 'NONE',  #1213 ) ;
#1191=FACE_OUTER_BOUND ( 'NONE', #2416, .T. ) ;
#1196=CARTESIAN_POINT ( 'NONE',  ( 3.384743657228182972E-15, 0.3911686820828953470, 4.000000000000003553 ) ) ;
#1213=AXIS2_PLACEMENT_3D ( 'NONE', #2212, #13258, #3452 ) ;
#1225=DIRECTION ( 'NONE',  ( -2.551526159633725302E-19, -1.000000000000000000, 4.440892098500621231E-16 ) ) ;
#1228=ORIENTED_EDGE ( 'NONE', *, *, #14399, .T. ) ;
#1238=ORIENTED_EDGE ( 'NONE', *, *, #2251, .T. ) ;
#1239=CARTESIAN_POINT ( 'NONE',  ( 0.000000000000000000, 0.000000000000000000, 0.000000000000000000 ) ) ;
#1245=AXIS2_PLACEMENT_3D ( 'NONE', #7766, #7833, #13 ) ;
#1263=CARTESIAN_POINT ( 'NONE',  ( 4.966173724562063185, -1.610348207484623817, 4.074842637297178882 ) ) ;
#1287=CARTESIAN_POINT ( 'NONE',  ( 5.551115123125782702E-14, 1.387778780781445676E-14, -4.000000000000003553 ) ) ;
#1304=CARTESIAN_POINT ( 'NONE',  ( 0.3572655899081733644, -4.618802153516988973, -1.387778780781445676E-14 ) ) ;
#1318=CARTESIAN_POINT ( 'NONE',  ( 4.851472949721049588, 4.233901974057263651, -0.6666666666666535290 ) ) ;
#1333=CARTESIAN_POINT ( 'NONE',  ( 5.103531824934115946, -2.354098498486438373, 4.077418205400141105 ) ) ;
#1343=EDGE_CURVE ( 'NONE', #6304, #2703, #7663, .T. ) ;
#1354=CARTESIAN_POINT ( 'NONE',  ( 8.178185494084536283E-16, 3.857556137907083293, -1.318516776095773224 ) ) ;
#1402=ORIENTED_EDGE ( 'NONE', *, *, #2494, .T. ) ;
#1413=CARTESIAN_POINT ( 'NONE',  ( 4.871660775260050258, 3.916561903058253691, 1.361048636879866658 ) ) ;
#1427=CARTESIAN_POINT ( 'NONE',  ( 5.013196232911400152, 4.621129290018668456, -2.362106518389725739E-18 ) ) ;
#1443=CARTESIAN_POINT ( 'NONE',  ( 0.3572655899081733644, 2.309401076758504701, -3.999999999999989786 ) ) ;
#1445=EDGE_CURVE ( 'NONE', #8503, #8261, #12465, .T. ) ;
#1454=ADVANCED_FACE ( 'NONE', ( #3639, #2066 ), #8789, .T. ) ;
#1464=PLANE ( 'NONE',  #12425 ) ;
#1488=UNCERTAINTY_MEASURE_WITH_UNIT (LENGTH_MEASURE( 1.000000000000000082E-05 ), #9973, 'distance_accuracy_value', 'NONE');
#1493=CARTESIAN_POINT ( 'NONE',  ( 5.005210506770622736, 2.400510894617556623, -4.000000000000002665 ) ) ;
#1504=CARTESIAN_POINT ( 'NONE',  ( 5.103531824934115946, -2.354098498486438373, 4.077418205400141105 ) ) ;
#1513=ORIENTED_EDGE ( 'NONE', *, *, #2251, .F. ) ;
#1526=ORIENTED_EDGE ( 'NONE', *, *, #58, .F. ) ;
#1550=AXIS2_PLACEMENT_3D ( 'NONE', #152, #7897, #11269 ) ;
#1561=ORIENTED_EDGE ( 'NONE', *, *, #14170, .T. ) ;
#1568=CARTESIAN_POINT ( 'NONE',  ( 5.085139881807307916, -4.657383176246346679, 0.06682429157518411655 ) ) ;
#1597=DIRECTION ( 'NONE',  ( 1.734723475976770694E-18, -4.440892098500621231E-16, -1.000000000000000000 ) ) ;
#1601=CARTESIAN_POINT ( 'NONE',  ( 5.067058822021066611, -2.325541950156887694, -4.027956812804548647 ) ) ;
#1602=FACE_OUTER_BOUND ( 'NONE', #12063, .T. ) ;
#1618=EDGE_LOOP ( 'NONE', ( #12820, #14405, #5969 ) ) ;
#1627=ORIENTED_EDGE ( 'NONE', *, *, #13810, .T. ) ;
#1631=CARTESIAN_POINT ( 'NONE',  ( 4.872568031907682951, -3.922980182067751898, 1.349977486297343043 ) ) ;
#1651=MECHANICAL_DESIGN_GEOMETRIC_PRESENTATION_REPRESENTATION('',(#14280),#3532);
#1682=CARTESIAN_POINT ( 'NONE',  ( 5.035982117295206173, -2.314736229921483535, -4.009240756344418344 ) ) ;
#1741=CARTESIAN_POINT ( 'NONE',  ( 4.960860176462274396, 1.574785417369866769, 4.074727069546279168 ) ) ;
#1756=DIRECTION ( 'NONE',  ( -1.000000000000000000, 2.551526159633733968E-19, 1.987661601597216239E-18 ) ) ;
#1766=CARTESIAN_POINT ( 'NONE',  ( 0.1391502195351279059, -2.687187980154724265, -3.345653888883624028 ) ) ;
#1777=VERTEX_POINT ( 'NONE', #5126 ) ;
#1791=( LENGTH_UNIT ( ) NAMED_UNIT ( * ) SI_UNIT ( .MILLI., .METRE. ) );
#1835=CARTESIAN_POINT ( 'NONE',  ( 5.733169058567799681, -9.797989565831383431E-15, -6.438111078829122036 ) ) ;
#1856=CARTESIAN_POINT ( 'NONE',  ( 1.057097118173367415E-15, -0.3908539631446322216, 4.000000000000004441 ) ) ;
#1869=ORIENTED_EDGE ( 'NONE', *, *, #9807, .F. ) ;
#1879=CARTESIAN_POINT ( 'NONE',  ( 5.091953023115930677, -2.341213539480237582, 4.055100801747969719 ) ) ;
#1915=CARTESIAN_POINT ( 'NONE',  ( 4.872112557124452792, -0.7838640816432008718, -4.072377784234222808 ) ) ;
#1922=ORIENTED_EDGE ( 'NONE', *, *, #4515, .T. ) ;
#1926=CARTESIAN_POINT ( 'NONE',  ( 4.988724804725896966, 2.309401076758504701, 4.000000000000031086 ) ) ;
#1942=( GEOMETRIC_REPRESENTATION_CONTEXT ( 3 ) GLOBAL_UNCERTAINTY_ASSIGNED_CONTEXT ( ( #12748 ) ) GLOBAL_UNIT_ASSIGNED_CONTEXT ( ( #1791, #9544, #8437 ) ) REPRESENTATION_CONTEXT ( 'NONE', 'WORKASPACE' ) );
#1944=CIRCLE ( 'NONE', #3354, 4.000000000000004441 ) ;
#1948=CARTESIAN_POINT ( 'NONE',  ( 4.851472949721052252, -1.539600717838985666, 4.000000000000002665 ) ) ;
#1957=CARTESIAN_POINT ( 'NONE',  ( 0.000000000000000000, 4.618802153517023612, 0.000000000000000000 ) ) ;
#1960=ADVANCED_FACE ( 'NONE', ( #5821 ), #6764, .T. ) ;
#1964=AXIS2_PLACEMENT_3D ( 'NONE', #13099, #5530, #8824 ) ;
#1968=ORIENTED_EDGE ( 'NONE', *, *, #1057, .F. ) ;
#1970=EDGE_LOOP ( 'NONE', ( #11011, #9719, #183, #4660, #1968 ) ) ;
#1994=B_SPLINE_CURVE_WITH_KNOTS ( 'NONE', 3,
 ( #9739, #2209, #11188, #8712, #10971, #8779 ),
 .UNSPECIFIED., .F., .F.,
 ( 4, 2, 4 ),
 ( 0.002336974151641544283, 0.003500975885716459297, 0.004664977619791374312 ),
 .UNSPECIFIED. ) ;
#2003=DIRECTION ( 'NONE',  ( 0.000000000000000000, 4.440892098500620738E-16, 1.000000000000000000 ) ) ;
#2022=DIRECTION ( 'NONE',  ( -1.000000000000000000, 2.551526159633733968E-19, 1.987661601597216239E-18 ) ) ;
#2026=CARTESIAN_POINT ( 'NONE',  ( 5.103531824934171013, 4.708196996972911386, -1.387778780781445676E-14 ) ) ;
#2044=AXIS2_PLACEMENT_3D ( 'NONE', #5674, #133, #6854 ) ;
#2056=CARTESIAN_POINT ( 'NONE',  ( 4.873329151231342138, 3.940175375302556127, -1.320232820537355245 ) ) ;
#2057=ORIENTED_EDGE ( 'NONE', *, *, #10089, .T. ) ;
#2066=FACE_OUTER_BOUND ( 'NONE', #4145, .T. ) ;
#2099=ADVANCED_FACE ( 'NONE', ( #10750 ), #10503, .T. ) ;
#2120=CARTESIAN_POINT ( 'NONE',  ( 4.988724804725896966, 2.309401076758504701, 4.000000000000031086 ) ) ;
#2155=CARTESIAN_POINT ( 'NONE',  ( 4.859338314252994451, 1.606026148912531593, 4.000000000000002665 ) ) ;
#2179=CARTESIAN_POINT ( 'NONE',  ( 4.960798468789972659, 4.316040323963743930, -0.6738506825564518632 ) ) ;
#2186=DIRECTION ( 'NONE',  ( -1.000000000000000000, 2.551526159633733968E-19, 1.987661601597216239E-18 ) ) ;
#2198=EDGE_LOOP ( 'NONE', ( #6287, #12200, #2341, #9735 ) ) ;
#2202=ORIENTED_EDGE ( 'NONE', *, *, #13155, .T. ) ;
#2209=CARTESIAN_POINT ( 'NONE',  ( 6.136753702857403984E-16, 3.660093687634858650, 1.660531772554304952 ) ) ;
#2212=CARTESIAN_POINT ( 'NONE',  ( 6.800000000000028244, 2.309401076758498039, 4.000000000000003553 ) ) ;
#2227=CARTESIAN_POINT ( 'NONE',  ( 4.873338085004320419, -0.8268058653460038654, 4.072408605319526309 ) ) ;
#2247=EDGE_LOOP ( 'NONE', ( #6228, #11523, #8280, #7267 ) ) ;
#2251=EDGE_CURVE ( 'NONE', #2725, #10176, #13782, .T. ) ;
#2255=VERTEX_POINT ( 'NONE', #926 ) ;
#2277=ORIENTED_EDGE ( 'NONE', *, *, #10866, .F. ) ;
#2285=CARTESIAN_POINT ( 'NONE',  ( 4.966167347451010627, -4.334074124826126528, 0.6428484488894387061 ) ) ;
#2290=CARTESIAN_POINT ( 'NONE',  ( 5.084394237956035845, 2.335963250529163204, 4.046007034530258117 ) ) ;
#2313=B_SPLINE_CURVE_WITH_KNOTS ( 'NONE', 3,
 ( #13775, #10460, #11630, #10175, #156, #9068 ),
 .UNSPECIFIED., .F., .F.,
 ( 4, 2, 4 ),
 ( 0.002336974151641542548, 0.003500975885716412026, 0.004664977619791281505 ),
 .UNSPECIFIED. ) ;
#2341=ORIENTED_EDGE ( 'NONE', *, *, #7099, .F. ) ;
#2343=AXIS2_PLACEMENT_3D ( 'NONE', #12678, #12529, #13580 ) ;
#2349=EDGE_CURVE ( 'NONE', #1777, #8228, #9032, .T. ) ;
#2352=COLOUR_RGB ( '', 0.72549020, 0.75294118, 0.79215686) ;
#2356=CARTESIAN_POINT ( 'NONE',  ( 4.870920456765270856, -3.129869081975100276, 2.723603336645685769 ) ) ;
#2359=EDGE_CURVE ( 'NONE', #8228, #11273, #5310, .T. ) ;
#2363=CARTESIAN_POINT ( 'NONE',  ( 5.103279350327357911, 2.353751664345929306, 4.076817471046935815 ) ) ;
#2383=ORIENTED_EDGE ( 'NONE', *, *, #5122, .F. ) ;
#2390=CARTESIAN_POINT ( 'NONE',  ( 0.000000000000000000, 2.081668171172168513E-14, 4.000000000000003553 ) ) ;
#2398=CARTESIAN_POINT ( 'NONE',  ( 6.250000000000033751, 9.714451465470119729E-15, 6.249999999999993783 ) ) ;
#2403=CARTESIAN_POINT ( 'NONE',  ( 4.960411150172048700, -1.572332708191213291, 4.074718599813436093 ) ) ;
#2404=CARTESIAN_POINT ( 'NONE',  ( 5.056385618527004411, -4.642911450026661058, -1.387778780781445676E-14 ) ) ;
#2416=EDGE_LOOP ( 'NONE', ( #10027, #9998, #5074, #10285, #11594 ) ) ;
#2432=EDGE_LOOP ( 'NONE', ( #6062, #4963, #12979 ) ) ;
#2450=CARTESIAN_POINT ( 'NONE',  ( 5.103531824934115946, 2.354098498486452584, 4.077418205400126894 ) ) ;
#2463=CARTESIAN_POINT ( 'NONE',  ( 1.210692425942146947E-15, -0.3908539631355372190, -4.000000000000004441 ) ) ;
#2486=DIRECTION ( 'NONE',  ( -1.000000000000000000, 2.551526159633717598E-19, -1.734723475976770887E-18 ) ) ;
#2494=EDGE_CURVE ( 'NONE', #10570, #5783, #6675, .T. ) ;
#2499=FACE_OUTER_BOUND ( 'NONE', #13157, .T. ) ;
#2509=CARTESIAN_POINT ( 'NONE',  ( 0.03458865240596911694, 0.7871057074556094824, -4.000000000000003553 ) ) ;
#2514=DIRECTION ( 'NONE',  ( 0.000000000000000000, -4.440892098500620245E-16, -1.000000000000000000 ) ) ;
#2523=( BOUNDED_SURFACE ( )  B_SPLINE_SURFACE ( 3, 2, ( 
 ( #12082, #14359, #7670 ),
 ( #6502, #6240, #12923 ),
 ( #11054, #9888, #2056 ),
 ( #10972, #5554, #8849 ),
 ( #947, #4489, #7340 ),
 ( #876, #5488, #11817 ) ),
 .UNSPECIFIED., .F., .F., .T. ) 
 B_SPLINE_SURFACE_WITH_KNOTS ( ( 4, 2, 4 ),
 ( 3, 3 ),
 ( 0.01886032586153034429, 0.02121253401777977582, 0.02356474217402920734 ),
 ( 0.000000000000000000, 1.000000000000000000 ),
 .UNSPECIFIED. ) 
 GEOMETRIC_REPRESENTATION_ITEM ( )  RATIONAL_B_SPLINE_SURFACE ( (
 ( 1.000000000000000000, 0.8047781103519396906, 1.000000000000000000),
 ( 1.000000000000000000, 0.8123785825774894054, 1.000000000000000000),
 ( 1.000000000000000000, 0.8190671539561196202, 1.000000000000000000),
 ( 1.000000000000000000, 0.8192352255061938759, 1.000000000000000000),
 ( 1.000000000000000000, 0.8126129677041067367, 1.000000000000000000),
 ( 1.000000000000000000, 0.8047712537969723412, 1.000000000000000000) ) ) 
 REPRESENTATION_ITEM ( '' )  SURFACE ( )  );
#2537=CARTESIAN_POINT ( 'NONE',  ( -5.551115123125782702E-14, 3.464101615137750390, -2.000000000000001776 ) ) ;
#2541=EDGE_CURVE ( 'NONE', #12769, #7655, #11233, .T. ) ;
#2544=CARTESIAN_POINT ( 'NONE',  ( 6.800000000000028244, 2.309401076758504701, -4.000000000000003553 ) ) ;
#2556=AXIS2_PLACEMENT_3D ( 'NONE', #8398, #1756, #726 ) ;
#2590=DIRECTION ( 'NONE',  ( 1.000000000000000000, -2.551526159633733968E-19, -1.987661601597216239E-18 ) ) ;
#2599=CARTESIAN_POINT ( 'NONE',  ( 4.844561581013297591, -3.861881939214885762, -1.311024268447341656 ) ) ;
#2601=CARTESIAN_POINT ( 'NONE',  ( 5.085139881807313245, 4.657383176246348455, -0.06682429157517222329 ) ) ;
#2639=CARTESIAN_POINT ( 'NONE',  ( 5.091953023115928900, 2.341213539480256234, 4.055100801747967054 ) ) ;
#2642=CONICAL_SURFACE ( 'NONE', #3578, 4.000000000000004441, 1.047197551196600296 ) ;
#2657=CARTESIAN_POINT ( 'NONE',  ( 5.084394237956035845, 2.335963250529156543, -4.046007034530243907 ) ) ;
#2685=CARTESIAN_POINT ( 'NONE',  ( 5.102759246810695259, 4.706121570500113371, -6.938893903907228378E-14 ) ) ;
#2689=CARTESIAN_POINT ( 'NONE',  ( 0.3572655899082288755, 4.618802153517023612, 1.387778780781445676E-14 ) ) ;
#2702=EDGE_CURVE ( 'NONE', #12991, #7983, #6334, .T. ) ;
#2703=VERTEX_POINT ( 'NONE', #5245 ) ;
#2713=CARTESIAN_POINT ( 'NONE',  ( 5.102759246810640192, -2.353060785250063347, -4.075620833351001338 ) ) ;
#2725=VERTEX_POINT ( 'NONE', #4588 ) ;
#2742=SURFACE_SIDE_STYLE ('',( #8211 ) ) ;
#2763=CARTESIAN_POINT ( 'NONE',  ( 0.1391502195351453364, 4.241015250120821811, -0.6543461111163241251 ) ) ;
#2764=ORIENTED_EDGE ( 'NONE', *, *, #3771, .F. ) ;
#2766=CARTESIAN_POINT ( 'NONE',  ( 0.1586754815284855125, -2.687817229851451994, 3.344563996438223885 ) ) ;
#2783=CIRCLE ( 'NONE', #196, 4.000000000000004441 ) ;
#2798=ORIENTED_EDGE ( 'NONE', *, *, #3771, .T. ) ;
#2812=B_SPLINE_CURVE_WITH_KNOTS ( 'NONE', 3,
 ( #11082, #1196, #7919, #6889, #6679, #12324 ),
 .UNSPECIFIED., .F., .F.,
 ( 4, 2, 4 ),
 ( 0.006655250997664750867, 0.007825277639709792357, 0.008995304281754833847 ),
 .UNSPECIFIED. ) ;
#2816=CARTESIAN_POINT ( 'NONE',  ( 0.3572655899081733644, 2.309401076758504701, -3.999999999999989786 ) ) ;
#2818=CARTESIAN_POINT ( 'NONE',  ( 0.03363697881402510914, -0.7786124122131015124, 4.000000000000004441 ) ) ;
#2849=CARTESIAN_POINT ( 'NONE',  ( 5.733169058567799681, -6.938893903907228378E-15, 0.000000000000000000 ) ) ;
#2863=TOROIDAL_SURFACE ( 'NONE', #4714, 6.250000000000000000, 0.5499999999999992673 ) ;
#2875=CARTESIAN_POINT ( 'NONE',  ( 0.3572655899080068309, -2.309401076758678339, -4.000000000000031086 ) ) ;
#2879=DIRECTION ( 'NONE',  ( -1.734723475976770502E-18, 4.440892098500621231E-16, 1.000000000000000000 ) ) ;
#2899=DIRECTION ( 'NONE',  ( 0.3420201433256618850, 5.322992421552529242E-16, 0.9396926207859108704 ) ) ;
#2989=ADVANCED_FACE ( 'NONE', ( #88 ), #2523, .F. ) ;
#3002=CIRCLE ( 'NONE', #12331, 4.000000000000004441 ) ;
#3021=CONICAL_SURFACE ( 'NONE', #6492, 6.438111078829122036, 1.221730476396037712 ) ;
#3027=EDGE_CURVE ( 'NONE', #630, #10570, #3438, .T. ) ;
#3046=CARTESIAN_POINT ( 'NONE',  ( 4.862825178850999741, 1.624847281681430111, -4.000000000000002665 ) ) ;
#3078=EDGE_LOOP ( 'NONE', ( #2383, #8611, #358, #12585, #5861, #6644 ) ) ;
#3106=ADVANCED_FACE ( 'NONE', ( #5692 ), #13480, .F. ) ;
#3115=CARTESIAN_POINT ( 'NONE',  ( 4.873320210002471953, 0.8266591206104413336, -4.072408155786487960 ) ) ;
#3190=DIRECTION ( 'NONE',  ( 1.734723475976770502E-18, -4.440892098500621231E-16, -1.000000000000000000 ) ) ;
#3197=EDGE_CURVE ( 'NONE', #5783, #630, #4084, .T. ) ;
#3218=CARTESIAN_POINT ( 'NONE',  ( 6.800000000000028244, 2.309401076758504701, -4.000000000000003553 ) ) ;
#3221=CARTESIAN_POINT ( 'NONE',  ( 5.103279350327408537, -4.707503328691831967, 2.873572379795871114E-14 ) ) ;
#3227=CIRCLE ( 'NONE', #7674, 3.000000000000003553 ) ;
#3248=CARTESIAN_POINT ( 'NONE',  ( 4.988724804725785944, -4.618802153517009401, 0.000000000000000000 ) ) ;
#3252=CARTESIAN_POINT ( 'NONE',  ( 31.24550000000003536, 1.332267629550187849E-15, 3.000000000000003553 ) ) ;
#3262=VECTOR ( 'NONE', #14029, 1000.000000000000000 ) ;
#3275=SURFACE_STYLE_USAGE ( .BOTH. , #1140 ) ;
#3277=CARTESIAN_POINT ( 'NONE',  ( 5.103531824934171013, 4.708196996972911386, -1.387778780781445676E-14 ) ) ;
#3282=ORIENTED_EDGE ( 'NONE', *, *, #13778, .F. ) ;
#3283=LINE ( 'NONE', #14192, #3834 ) ;
#3299=CARTESIAN_POINT ( 'NONE',  ( 4.686019787951574145, 3.464101615137745060, 2.000000000000011990 ) ) ;
#3327=CARTESIAN_POINT ( 'NONE',  ( 4.769962962078704294, -3.881286623615096687, 1.277414369161164798 ) ) ;
#3329=DIRECTION ( 'NONE',  ( -1.000000000000000000, 2.551526159633733968E-19, 1.987661601597216239E-18 ) ) ;
#3352=AXIS2_PLACEMENT_3D ( 'NONE', #14386, #11295, #5779 ) ;
#3354=AXIS2_PLACEMENT_3D ( 'NONE', #14003, #8637, #2879 ) ;
#3356=DIRECTION ( 'NONE',  ( -1.000000000000000000, 2.551526159633733968E-19, 1.987661601597216239E-18 ) ) ;
#3375=CARTESIAN_POINT ( 'NONE',  ( 5.084394237956035845, -4.671926501058319303, -1.387778780781445676E-14 ) ) ;
#3386=EDGE_CURVE ( 'NONE', #8457, #11273, #14423, .T. ) ;
#3404=ADVANCED_FACE ( 'NONE', ( #10915 ), #889, .T. ) ;
#3406=B_SPLINE_CURVE_WITH_KNOTS ( 'NONE', 3,
 ( #10752, #5189, #12726, #2713, #7147, #8553, #9511, #11623, #1601, #12798, #515, #1682, #13914, #8400, #12879, #3885 ),
 .UNSPECIFIED., .F., .F.,
 ( 4, 3, 3, 3, 3, 4 ),
 ( -2.214559098585470453E-06, 0.000000000000000000, 3.881464059292277384E-05, 7.921402936568253800E-05, 0.0001155901529638105323, 0.0001522174276056047432 ),
 .UNSPECIFIED. ) ;
#3407=CARTESIAN_POINT ( 'NONE',  ( 4.988724804725896966, 2.309401076758504701, 4.000000000000031086 ) ) ;
#3438=CIRCLE ( 'NONE', #4149, 4.000000000000004441 ) ;
#3452=DIRECTION ( 'NONE',  ( -8.138903065828892551E-32, 1.000000000000000000, 7.771561172376088880E-16 ) ) ;
#3470=CARTESIAN_POINT ( 'NONE',  ( 5.046772446839278281, 2.317775331972814268, 4.014504635506723318 ) ) ;
#3496=EDGE_CURVE ( 'NONE', #4363, #6994, #9478, .T. ) ;
#3498=ORIENTED_EDGE ( 'NONE', *, *, #13558, .T. ) ;
#3532=( GEOMETRIC_REPRESENTATION_CONTEXT ( 3 ) GLOBAL_UNCERTAINTY_ASSIGNED_CONTEXT ( ( #9683 ) ) GLOBAL_UNIT_ASSIGNED_CONTEXT ( ( #4317, #8960, #7790 ) ) REPRESENTATION_CONTEXT ( 'NONE', 'WORKASPACE' ) );
#3548=CARTESIAN_POINT ( 'NONE',  ( 5.103021810857248042, 2.353405741491033876, -4.076218315086673982 ) ) ;
#3572=CARTESIAN_POINT ( 'NONE',  ( 4.767554269344628004, -3.864655694377453266, -1.306219983577875832 ) ) ;
#3578=AXIS2_PLACEMENT_3D ( 'NONE', #8710, #1165, #6574 ) ;
#3586=CARTESIAN_POINT ( 'NONE',  ( 5.103531824934115946, -2.354098498486438373, 4.077418205400141105 ) ) ;
#3595=CARTESIAN_POINT ( 'NONE',  ( 4.872112557122744825, -2.415761400130177830E-11, -4.072377784234180176 ) ) ;
#3598=CIRCLE ( 'NONE', #1245, 6.250000000000007105 ) ;
#3617=CARTESIAN_POINT ( 'NONE',  ( 5.067058822021063058, 2.325541950156893911, -4.027956812804547759 ) ) ;
#3618=ORIENTED_EDGE ( 'NONE', *, *, #3197, .F. ) ;
#3636=CARTESIAN_POINT ( 'NONE',  ( 5.005210273051230452, -2.263846804438352844, -4.078902314160335330 ) ) ;
#3639=FACE_BOUND ( 'NONE', #10061, .T. ) ;
#3643=CARTESIAN_POINT ( 'NONE',  ( 0.2486750293958585323, -1.933232340699151397, -4.000000000000002665 ) ) ;
#3691=AXIS2_PLACEMENT_3D ( 'NONE', #8624, #11032, #6635 ) ;
#3695=B_SPLINE_CURVE_WITH_KNOTS ( 'NONE', 3,
 ( #11378, #12487, #5670, #11451, #11240, #9105 ),
 .UNSPECIFIED., .F., .F.,
 ( 4, 2, 4 ),
 ( 0.000000000000000000, 0.002383230369971167488, 0.004766460739942334109 ),
 .UNSPECIFIED. ) ;
#3701=CARTESIAN_POINT ( 'NONE',  ( 4.851472949720938566, -4.233901974057253881, 0.6666666666666709595 ) ) ;
#3710=CARTESIAN_POINT ( 'NONE',  ( 5.046772446839293380, 4.635550663945619654, -3.696590807480215359E-18 ) ) ;
#3716=CARTESIAN_POINT ( 'NONE',  ( 4.988724804725896966, -2.309401076758484272, 4.000000000000003553 ) ) ;
#3738=DIRECTION ( 'NONE',  ( 1.000000000000000000, -2.551526159633733968E-19, -1.987661601597216239E-18 ) ) ;
#3771=EDGE_CURVE ( 'NONE', #13637, #8706, #451, .T. ) ;
#3776=CARTESIAN_POINT ( 'NONE',  ( 5.108705940669685752, -4.722350143107945541, 0.02431935820581593993 ) ) ;
#3827=APPLICATION_CONTEXT ( 'automotive_design' ) ;
#3834=VECTOR ( 'NONE', #2186, 1000.000000000000000 ) ;
#3835=VERTEX_POINT ( 'NONE', #7992 ) ;
#3841=EDGE_LOOP ( 'NONE', ( #4223, #4838, #6224, #9368 ) ) ;
#3858=CARTESIAN_POINT ( 'NONE',  ( 4.862831555539507633, -2.651660758729945666, -3.407188841443101524 ) ) ;
#3859=CARTESIAN_POINT ( 'NONE',  ( 5.108705940669691969, 4.722350143107947318, -0.02431935820580391483 ) ) ;
#3860=CARTESIAN_POINT ( 'NONE',  ( 5.076540720129197659, 4.661016483905926044, -1.388525000602713847E-14 ) ) ;
#3871=CARTESIAN_POINT ( 'NONE',  ( 4.872112557121027976, -0.7881298154075988549, 4.072377784234137543 ) ) ;
#3885=CARTESIAN_POINT ( 'NONE',  ( 4.988724804725785944, -2.309401076758511806, -3.999999999999989786 ) ) ;
#3907=CARTESIAN_POINT ( 'NONE',  ( 0.1597025669805195447, 1.557591170365174804, -4.000000000000004441 ) ) ;
#3927=CARTESIAN_POINT ( 'NONE',  ( 4.767554269344989493, 3.864655694377410189, 1.306219983577960209 ) ) ;
#3932=B_SPLINE_CURVE_WITH_KNOTS ( 'NONE', 3,
 ( #6571, #12013, #1915, #8915 ),
 .UNSPECIFIED., .F., .F.,
 ( 4, 4 ),
 ( 0.000000000000000000, 0.002376763279741518631 ),
 .UNSPECIFIED. ) ;
#3938=CARTESIAN_POINT ( 'NONE',  ( 5.551115123125782702E-14, -3.464101615137743728, 2.000000000000001776 ) ) ;
#3966=LINE ( 'NONE', #1835, #12449 ) ;
#4010=ORIENTED_EDGE ( 'NONE', *, *, #13678, .T. ) ;
#4026=ORIENTED_EDGE ( 'NONE', *, *, #6151, .F. ) ;
#4084=B_SPLINE_CURVE_WITH_KNOTS ( 'NONE', 3,
 ( #9748, #7335, #11955, #2818, #1856, #763 ),
 .UNSPECIFIED., .F., .F.,
 ( 4, 2, 4 ),
 ( 0.004317080428420414645, 0.005486165713042582756, 0.006655250997664750867 ),
 .UNSPECIFIED. ) ;
#4085=FACE_OUTER_BOUND ( 'NONE', #2198, .T. ) ;
#4127=EDGE_LOOP ( 'NONE', ( #8029, #770, #8543, #2764 ) ) ;
#4137=ORIENTED_EDGE ( 'NONE', *, *, #4806, .F. ) ;
#4144=CARTESIAN_POINT ( 'NONE',  ( 4.769954020850214249, 0.8342959359879871251, -4.000000000000002665 ) ) ;
#4145=EDGE_LOOP ( 'NONE', ( #6323, #11922 ) ) ;
#4149=AXIS2_PLACEMENT_3D ( 'NONE', #7825, #8780, #5626 ) ;
#4151=CARTESIAN_POINT ( 'NONE',  ( 4.851472949721052252, -2.694301256218235796, 3.333333333333339699 ) ) ;
#4157=ORIENTED_EDGE ( 'NONE', *, *, #4348, .F. ) ;
#4162=CARTESIAN_POINT ( 'NONE',  ( 5.046772446839306703, -2.317775331972796504, 4.014504635506726871 ) ) ;
#4166=CARTESIAN_POINT ( 'NONE',  ( 6.800000000000028244, -9.697272942313059056E-16, -3.000000000000000000 ) ) ;
#4170=ADVANCED_FACE ( 'NONE', ( #4434 ), #5514, .F. ) ;
#4215=( NAMED_UNIT ( * ) PLANE_ANGLE_UNIT ( ) SI_UNIT ( $, .RADIAN. ) );
#4223=ORIENTED_EDGE ( 'NONE', *, *, #4804, .F. ) ;
#4246=EDGE_CURVE ( 'NONE', #8503, #3835, #6377, .T. ) ;
#4291=DIRECTION ( 'NONE',  ( -1.000000000000000000, 2.551526159633733968E-19, 1.987661601597216239E-18 ) ) ;
#4312=PLANE ( 'NONE',  #6074 ) ;
#4317=( LENGTH_UNIT ( ) NAMED_UNIT ( * ) SI_UNIT ( .MILLI., .METRE. ) );
#4348=EDGE_CURVE ( 'NONE', #630, #7481, #1944, .T. ) ;
#4355=CARTESIAN_POINT ( 'NONE',  ( 4.686019787951672733, -3.464101615137762380, -1.999999999999994893 ) ) ;
#4356=CARTESIAN_POINT ( 'NONE',  ( 5.108576461337678509, -4.721997478884301991, -0.02371338167649895967 ) ) ;
#4363=VERTEX_POINT ( 'NONE', #5125 ) ;
#4367=CARTESIAN_POINT ( 'NONE',  ( 5.103531824934171013, -4.708196996972898063, 1.387778780781445676E-14 ) ) ;
#4385=DIRECTION ( 'NONE',  ( 1.000000000000000000, -2.551526159633733968E-19, -1.987661601597216239E-18 ) ) ;
#4431=DIRECTION ( 'NONE',  ( 1.000000000000000000, -2.551526159633717598E-19, 1.734723475976770887E-18 ) ) ;
#4434=FACE_OUTER_BOUND ( 'NONE', #4127, .T. ) ;
#4438=EDGE_CURVE ( 'NONE', #10176, #6205, #13330, .T. ) ;
#4439=CARTESIAN_POINT ( 'NONE',  ( 4.862837926274030664, -1.624916111836509858, 4.000000000000003553 ) ) ;
#4463=ORIENTED_EDGE ( 'NONE', *, *, #13859, .T. ) ;
#4478=ADVANCED_FACE ( 'NONE', ( #1026 ), #2642, .T. ) ;
#4489=CARTESIAN_POINT ( 'NONE',  ( 4.939003118778963142, 2.662716476701372681, -3.388039776202472098 ) ) ;
#4515=EDGE_CURVE ( 'NONE', #6994, #7481, #4739, .T. ) ;
#4551=ORIENTED_EDGE ( 'NONE', *, *, #58, .T. ) ;
#4577=CARTESIAN_POINT ( 'NONE',  ( 5.085140069777600580, 2.386564130380674165, 4.000000000000002665 ) ) ;
#4588=CARTESIAN_POINT ( 'NONE',  ( 31.80000000000005045, 6.063261456088593708E-15, -2.445499999999972474 ) ) ;
#4598=ORIENTED_EDGE ( 'NONE', *, *, #12458, .F. ) ;
#4614=EDGE_CURVE ( 'NONE', #14288, #568, #5133, .T. ) ;
#4622=AXIS2_PLACEMENT_3D ( 'NONE', #2398, #1225, #7873 ) ;
#4659=CARTESIAN_POINT ( 'NONE',  ( 5.108576461337681174, -2.340462348500684353, -4.101226464158124863 ) ) ;
#4660=ORIENTED_EDGE ( 'NONE', *, *, #522, .F. ) ;
#4665=ORIENTED_EDGE ( 'NONE', *, *, #13305, .F. ) ;
#4688=CARTESIAN_POINT ( 'NONE',  ( 5.551115123125782702E-14, -3.464101615137743728, 2.000000000000001776 ) ) ;
#4694=LINE ( 'NONE', #9364, #13633 ) ;
#4706=CARTESIAN_POINT ( 'NONE',  ( 0.000000000000000000, 0.000000000000000000, 0.000000000000000000 ) ) ;
#4714=AXIS2_PLACEMENT_3D ( 'NONE', #5268, #11858, #7313 ) ;
#4739=CIRCLE ( 'NONE', #302, 4.000000000000004441 ) ;
#4764=ADVANCED_FACE ( 'NONE', ( #13225 ), #4312, .F. ) ;
#4768=ORIENTED_EDGE ( 'NONE', *, *, #7085, .T. ) ;
#4774=B_SPLINE_CURVE_WITH_KNOTS ( 'NONE', 3,
 ( #13786, #11571, #3548, #13713, #8122, #12744, #2657, #386, #3617, #5926, #9455, #5847, #8202, #6887, #316, #11647 ),
 .UNSPECIFIED., .F., .F.,
 ( 4, 3, 3, 3, 3, 4 ),
 ( -2.214559098553098548E-06, 0.000000000000000000, 3.881464059293194212E-05, 7.921402936568228050E-05, 0.0001155901529638607309, 0.0001522174276055590983 ),
 .UNSPECIFIED. ) ;
#4787=FACE_OUTER_BOUND ( 'NONE', #9061, .T. ) ;
#4797=CARTESIAN_POINT ( 'NONE',  ( 4.942464816486673129, 2.653516201069836988, 3.403975121041074026 ) ) ;
#4799=CARTESIAN_POINT ( 'NONE',  ( 5.035982117295163540, 4.629472459842971510, 2.352375968396500403E-18 ) ) ;
#4804=EDGE_CURVE ( 'NONE', #8584, #9446, #6536, .T. ) ;
#4805=CARTESIAN_POINT ( 'NONE',  ( 0.3572655899081733644, -2.309401076758484272, 4.000000000000031086 ) ) ;
#4806=EDGE_CURVE ( 'NONE', #6304, #5931, #13085, .T. ) ;
#4807=CARTESIAN_POINT ( 'NONE',  ( 4.872112557122744825, 2.415041619695410755E-11, 4.072377784234180176 ) ) ;
#4838=ORIENTED_EDGE ( 'NONE', *, *, #12526, .T. ) ;
#4844=DIRECTION ( 'NONE',  ( -1.000000000000000000, 2.551526159633733968E-19, 1.987661601597216239E-18 ) ) ;
#4848=CARTESIAN_POINT ( 'NONE',  ( 0.2494252716045076701, 1.935831255945836604, -4.000000000000003553 ) ) ;
#4862=CARTESIAN_POINT ( 'NONE',  ( 4.847001880572340049, -3.049720480807998513, -2.717729178357026321 ) ) ;
#4868=CARTESIAN_POINT ( 'NONE',  ( 5.000882498481359129, 4.618802153517016507, 1.397365476814232024E-14 ) ) ;
#4885=EDGE_LOOP ( 'NONE', ( #5301, #1513 ) ) ;
#4897=CARTESIAN_POINT ( 'NONE',  ( 5.103531824934115946, 2.354098498486452584, 4.077418205400126894 ) ) ;
#4920=B_SPLINE_CURVE_WITH_KNOTS ( 'NONE', 3,
 ( #3716, #11600, #10510, #4949, #842, #4162, #5242, #12945, #14248, #14043, #1879, #13161, #13959, #9632, #10805, #9769 ),
 .UNSPECIFIED., .F., .F.,
 ( 4, 3, 3, 3, 3, 4 ),
 ( 0.000000000000000000, 3.647308126642952050E-05, 7.269606878413157171E-05, 0.0001129253843484943226, 0.0001515766232005118122, 0.0001537911822990430675 ),
 .UNSPECIFIED. ) ;
#4928=CARTESIAN_POINT ( 'NONE',  ( 0.000000000000000000, 0.000000000000000000, 0.000000000000000000 ) ) ;
#4937=ORIENTED_EDGE ( 'NONE', *, *, #11603, .F. ) ;
#4938=CARTESIAN_POINT ( 'NONE',  ( 6.800000000000028244, 4.898485791573355875E-15, -6.250000000000000000 ) ) ;
#4941=CARTESIAN_POINT ( 'NONE',  ( 5.108576461337683838, 2.340462348500683021, 4.101226464158124863 ) ) ;
#4949=CARTESIAN_POINT ( 'NONE',  ( 5.024612689793206854, -2.312654742478263525, 4.005635514337482661 ) ) ;
#4963=ORIENTED_EDGE ( 'NONE', *, *, #8310, .T. ) ;
#4980=DIRECTION ( 'NONE',  ( 0.3420201433256618850, -4.173946208010309292E-16, -0.9396926207859108704 ) ) ;
#5020=CARTESIAN_POINT ( 'NONE',  ( 5.091953023115830312, 4.682427078960528455, -1.387060565653463815E-14 ) ) ;
#5061=ORIENTED_EDGE ( 'NONE', *, *, #2541, .T. ) ;
#5074=ORIENTED_EDGE ( 'NONE', *, *, #2541, .F. ) ;
#5076=LINE ( 'NONE', #9551, #3262 ) ;
#5084=CARTESIAN_POINT ( 'NONE',  ( 5.103021810857300444, 4.706811482981981598, -7.866781916910138702E-14 ) ) ;
#5118=CIRCLE ( 'NONE', #208, 6.250000000000007105 ) ;
#5120=ADVANCED_FACE ( 'NONE', ( #4787 ), #3021, .T. ) ;
#5122=EDGE_CURVE ( 'NONE', #47, #6994, #1124, .T. ) ;
#5125=CARTESIAN_POINT ( 'NONE',  ( 0.3572655899082288755, 4.618802153517023612, 1.387778780781445676E-14 ) ) ;
#5126=CARTESIAN_POINT ( 'NONE',  ( 6.800000000000028244, -4.163336342344337027E-15, 6.250000000000007105 ) ) ;
#5133=B_SPLINE_CURVE_WITH_KNOTS ( 'NONE', 3,
 ( #3595, #13627, #12506, #5820 ),
 .UNSPECIFIED., .F., .F.,
 ( 4, 4 ),
 ( 0.002376763279741518631, 0.004766460739942336711 ),
 .UNSPECIFIED. ) ;
#5150=ADVANCED_FACE ( 'NONE', ( #6963 ), #6995, .F. ) ;
#5158=CARTESIAN_POINT ( 'NONE',  ( 0.000000000000000000, 0.000000000000000000, 0.000000000000000000 ) ) ;
#5189=CARTESIAN_POINT ( 'NONE',  ( 5.103279350327459163, -2.353751664345928862, -4.076817471046940256 ) ) ;
#5223=SHAPE_REPRESENTATION_RELATIONSHIP ( 'NONE' , 'NONE' ,  #8802, #10106 ) ;
#5227=AXIS2_PLACEMENT_3D ( 'NONE', #5158, #832, #14030 ) ;
#5236=PRODUCT_DEFINITION_FORMATION_WITH_SPECIFIED_SOURCE ( 'ANY', '', #11275, .NOT_KNOWN. ) ;
#5242=CARTESIAN_POINT ( 'NONE',  ( 5.056385618527004411, -2.321455725013320315, 4.020879263244736990 ) ) ;
#5245=CARTESIAN_POINT ( 'NONE',  ( 4.988724804725785944, -4.618802153517009401, 0.000000000000000000 ) ) ;
#5266=PRODUCT_CONTEXT ( 'NONE', #3827, 'mechanical' ) ;
#5268=CARTESIAN_POINT ( 'NONE',  ( 6.250000000000033751, 6.938893903907228378E-15, -1.387778780781445676E-14 ) ) ;
#5278=ADVANCED_FACE ( 'NONE', ( #966 ), #6761, .T. ) ;
#5301=ORIENTED_EDGE ( 'NONE', *, *, #14246, .F. ) ;
#5310=CIRCLE ( 'NONE', #2044, 6.438111078829122036 ) ;
#5365=ORIENTED_EDGE ( 'NONE', *, *, #4614, .F. ) ;
#5378=DIRECTION ( 'NONE',  ( 1.000000000000000000, -2.551526159633717598E-19, 1.734723475976770887E-18 ) ) ;
#5414=DIRECTION ( 'NONE',  ( 1.734723475976770502E-18, -4.440892098500621231E-16, -1.000000000000000000 ) ) ;
#5433=CARTESIAN_POINT ( 'NONE',  ( 6.250000000000033751, 4.928740591811433280E-15, -6.250000000000021316 ) ) ;
#5441=DIRECTION ( 'NONE',  ( 1.000000000000000000, 0.000000000000000000, 0.000000000000000000 ) ) ;
#5459=CARTESIAN_POINT ( 'NONE',  ( 0.000000000000000000, 0.000000000000000000, 0.000000000000000000 ) ) ;
#5470=CARTESIAN_POINT ( 'NONE',  ( 31.80000000000005045, 6.938893903907228378E-15, 2.775557561562891351E-14 ) ) ;
#5488=CARTESIAN_POINT ( 'NONE',  ( 5.085139881807305251, 2.270820054029174528, -4.066824291575160899 ) ) ;
#5514=( BOUNDED_SURFACE ( )  B_SPLINE_SURFACE ( 3, 2, ( 
 ( #12313, #9900, #4356 ),
 ( #12383, #13350, #2285 ),
 ( #3327, #5637, #7771 ),
 ( #8791, #12244, #2356 ),
 ( #6814, #13273, #5766 ),
 ( #11636, #8045, #13708 ) ),
 .UNSPECIFIED., .F., .F., .F. ) 
 B_SPLINE_SURFACE_WITH_KNOTS ( ( 4, 2, 4 ),
 ( 3, 3 ),
 ( 0.01886032586153030266, 0.02121253401777973419, 0.02356474217402916571 ),
 ( 0.000000000000000000, 1.000000000000000000 ),
 .UNSPECIFIED. ) 
 GEOMETRIC_REPRESENTATION_ITEM ( )  RATIONAL_B_SPLINE_SURFACE ( (
 ( 1.000000000000000000, 0.8047781103519395796, 1.000000000000000000),
 ( 1.000000000000000000, 0.8123785825777626313, 1.000000000000000000),
 ( 1.000000000000000000, 0.8190671539557564662, 1.000000000000000000),
 ( 1.000000000000000000, 0.8192352255065570299, 1.000000000000000000),
 ( 1.000000000000000000, 0.8126129677038341770, 1.000000000000000000),
 ( 1.000000000000000000, 0.8047712537969725632, 1.000000000000000000) ) ) 
 REPRESENTATION_ITEM ( '' )  SURFACE ( )  );
#5515=CARTESIAN_POINT ( 'NONE',  ( 0.1391502195351393967, 2.687187980154705613, 3.345653888883665772 ) ) ;
#5524=CARTESIAN_POINT ( 'NONE',  ( 5.103531824934171013, 2.354098498486459246, -4.077418205400141105 ) ) ;
#5530=DIRECTION ( 'NONE',  ( -1.000000000000000000, 2.551526159633733968E-19, 1.987661601597216239E-18 ) ) ;
#5554=CARTESIAN_POINT ( 'NONE',  ( 4.844561581013301144, 3.066321291060833065, -2.688975731552607940 ) ) ;
#5563=VECTOR ( 'NONE', #10806, 1000.000000000000000 ) ;
#5564=CARTESIAN_POINT ( 'NONE',  ( 31.80000000000005045, 6.938893903907228378E-15, 2.775557561562891351E-14 ) ) ;
#5572=CARTESIAN_POINT ( 'NONE',  ( 4.844552896834077416, 0.7953914966942765563, 4.000000000000002665 ) ) ;
#5573=ORIENTED_EDGE ( 'NONE', *, *, #9596, .F. ) ;
#5616=ORIENTED_EDGE ( 'NONE', *, *, #11024, .F. ) ;
#5621=CARTESIAN_POINT ( 'NONE',  ( 31.80000000000005045, 8.024914066595556114E-15, 2.445500000000030649 ) ) ;
#5626=DIRECTION ( 'NONE',  ( 1.734723475976770502E-18, -4.440892098500621231E-16, -1.000000000000000000 ) ) ;
#5637=CARTESIAN_POINT ( 'NONE',  ( 4.847001880571981225, -3.878482749467707880, 1.282270821642251368 ) ) ;
#5642=CARTESIAN_POINT ( 'NONE',  ( 4.847010933397505106, -0.8288363800944087423, 4.000000000000002665 ) ) ;
#5670=CARTESIAN_POINT ( 'NONE',  ( 4.871660775260041376, -3.916561903058248806, -1.361048636879858664 ) ) ;
#5674=CARTESIAN_POINT ( 'NONE',  ( 5.733169058567799681, -6.938893903907228378E-15, 0.000000000000000000 ) ) ;
#5684=VECTOR ( 'NONE', #13740, 1000.000000000000000 ) ;
#5691=PLANE ( 'NONE',  #7957 ) ;
#5692=FACE_OUTER_BOUND ( 'NONE', #5984, .T. ) ;
#5695=ORIENTED_EDGE ( 'NONE', *, *, #3496, .F. ) ;
#5698=EDGE_LOOP ( 'NONE', ( #2057, #5573, #12944, #5970 ) ) ;
#5739=CARTESIAN_POINT ( 'NONE',  ( 31.24550000000003536, 0.000000000000000000, 0.000000000000000000 ) ) ;
#5766=CARTESIAN_POINT ( 'NONE',  ( 4.962664318264591756, -2.733102959025379253, 3.415681285063929984 ) ) ;
#5779=DIRECTION ( 'NONE',  ( 0.000000000000000000, 4.440892098500620738E-16, 1.000000000000000000 ) ) ;
#5783=VERTEX_POINT ( 'NONE', #4805 ) ;
#5802=AXIS2_PLACEMENT_3D ( 'NONE', #9902, #3329, #2003 ) ;
#5809=AXIS2_PLACEMENT_3D ( 'NONE', #5470, #11925, #8829 ) ;
#5814=EDGE_CURVE ( 'NONE', #8390, #13637, #4920, .T. ) ;
#5815=ORIENTED_EDGE ( 'NONE', *, *, #7480, .T. ) ;
#5817=ORIENTED_EDGE ( 'NONE', *, *, #1343, .T. ) ;
#5820=CARTESIAN_POINT ( 'NONE',  ( 5.103531824934171013, 2.354098498486459246, -4.077418205400141105 ) ) ;
#5821=FACE_OUTER_BOUND ( 'NONE', #1618, .T. ) ;
#5847=CARTESIAN_POINT ( 'NONE',  ( 5.035982117295162652, 2.314736229921479094, -4.009240756344450318 ) ) ;
#5861=ORIENTED_EDGE ( 'NONE', *, *, #4348, .T. ) ;
#5873=CARTESIAN_POINT ( 'NONE',  ( 5.024612689793150899, 4.625309484956555472, 0.000000000000000000 ) ) ;
#5878=( BOUNDED_SURFACE ( )  B_SPLINE_SURFACE ( 3, 2, ( 
 ( #10159, #142, #4941 ),
 ( #11669, #4797, #10502 ),
 ( #9482, #9557, #11521 ),
 ( #3927, #8371, #14034 ),
 ( #9402, #12849, #10654 ),
 ( #13884, #2601, #3859 ) ),
 .UNSPECIFIED., .F., .F., .F. ) 
 B_SPLINE_SURFACE_WITH_KNOTS ( ( 4, 2, 4 ),
 ( 3, 3 ),
 ( 0.01886032586153035123, 0.02121253401777978276, 0.02356474217402921081 ),
 ( 0.000000000000000000, 1.000000000000000000 ),
 .UNSPECIFIED. ) 
 GEOMETRIC_REPRESENTATION_ITEM ( )  RATIONAL_B_SPLINE_SURFACE ( (
 ( 1.000000000000000000, 0.8047781103519388024, 1.000000000000000000),
 ( 1.000000000000000000, 0.8123785825777287695, 1.000000000000000000),
 ( 1.000000000000000000, 0.8190671539558022074, 1.000000000000000000),
 ( 1.000000000000000000, 0.8192352255065119548, 1.000000000000000000),
 ( 1.000000000000000000, 0.8126129677038673726, 1.000000000000000000),
 ( 1.000000000000000000, 0.8047712537969721192, 1.000000000000000000) ) ) 
 REPRESENTATION_ITEM ( '' )  SURFACE ( )  );
#5879=STYLED_ITEM ( 'NONE', ( #13210 ), #10106 ) ;
#5892=CARTESIAN_POINT ( 'NONE',  ( -5.551115123125782702E-14, 3.464101615137750390, -2.000000000000001776 ) ) ;
#5908=CARTESIAN_POINT ( 'NONE',  ( 4.870911883258405517, 0.7936069845605383533, 4.072347588220287307 ) ) ;
#5926=CARTESIAN_POINT ( 'NONE',  ( 5.056385618527004411, 2.321455725013334082, -4.020879263244736990 ) ) ;
#5929=FACE_OUTER_BOUND ( 'NONE', #9836, .T. ) ;
#5931=VERTEX_POINT ( 'NONE', #11007 ) ;
#5935=CARTESIAN_POINT ( 'NONE',  ( 5.085009278891528872, 2.385862568036605680, -4.000000000000002665 ) ) ;
#5969=ORIENTED_EDGE ( 'NONE', *, *, #5122, .T. ) ;
#5970=ORIENTED_EDGE ( 'NONE', *, *, #13558, .F. ) ;
#5979=CARTESIAN_POINT ( 'NONE',  ( 4.962672901883133036, 1.591562006530089723, 4.074777397737123330 ) ) ;
#5984=EDGE_LOOP ( 'NONE', ( #13991, #1228, #7284, #7010, #2277 ) ) ;
#5997=DIRECTION ( 'NONE',  ( 1.987661601597216239E-18, 4.440892098500621724E-16, 1.000000000000000000 ) ) ;
#6030=CARTESIAN_POINT ( 'NONE',  ( 0.3572655899081733644, -2.309401076758484272, 4.000000000000031086 ) ) ;
#6041=APPLICATION_CONTEXT ( 'automotive_design' ) ;
#6062=ORIENTED_EDGE ( 'NONE', *, *, #13361, .T. ) ;
#6074=AXIS2_PLACEMENT_3D ( 'NONE', #1957, #5378, #1597 ) ;
#6085=CARTESIAN_POINT ( 'NONE',  ( 4.988724804725841011, 2.309401076758504701, -4.000000000000003553 ) ) ;
#6115=ADVANCED_FACE ( 'NONE', ( #8209 ), #9163, .F. ) ;
#6151=EDGE_CURVE ( 'NONE', #7655, #8228, #12996, .T. ) ;
#6205=VERTEX_POINT ( 'NONE', #3252 ) ;
#6217=CARTESIAN_POINT ( 'NONE',  ( -3.074732204440936414E-15, -3.070647092368440134, -2.681483223904212121 ) ) ;
#6224=ORIENTED_EDGE ( 'NONE', *, *, #756, .T. ) ;
#6228=ORIENTED_EDGE ( 'NONE', *, *, #12813, .T. ) ;
#6240=CARTESIAN_POINT ( 'NONE',  ( 4.942464816487918355, 4.274687029205021638, -0.5960248789591272578 ) ) ;
#6287=ORIENTED_EDGE ( 'NONE', *, *, #13778, .T. ) ;
#6304=VERTEX_POINT ( 'NONE', #13353 ) ;
#6321=ADVANCED_FACE ( 'NONE', ( #9821 ), #11426, .T. ) ;
#6323=ORIENTED_EDGE ( 'NONE', *, *, #7480, .F. ) ;
#6334=LINE ( 'NONE', #6405, #5563 ) ;
#6364=CARTESIAN_POINT ( 'NONE',  ( 5.551115123125782702E-14, 1.387778780781445676E-14, -4.000000000000003553 ) ) ;
#6377=B_SPLINE_CURVE_WITH_KNOTS ( 'NONE', 3,
 ( #10398, #1318, #11347, #379, #9072 ),
 .UNSPECIFIED., .F., .F.,
 ( 4, 1, 4 ),
 ( 0.000000000000000000, 0.002309401076758504923, 0.004618802153517009845 ),
 .UNSPECIFIED. ) ;
#6405=CARTESIAN_POINT ( 'NONE',  ( 6.800000000000028244, 2.309401076758498039, 4.000000000000003553 ) ) ;
#6449=ORIENTED_EDGE ( 'NONE', *, *, #3027, .T. ) ;
#6489=FACE_OUTER_BOUND ( 'NONE', #838, .T. ) ;
#6492=AXIS2_PLACEMENT_3D ( 'NONE', #9314, #249, #2514 ) ;
#6495=CARTESIAN_POINT ( 'NONE',  ( 4.851472949721050476, 2.694301256218257112, 3.333333333333363679 ) ) ;
#6502=CARTESIAN_POINT ( 'NONE',  ( 4.862831555538840611, 4.276542471545668356, -0.5928111585567288344 ) ) ;
#6503=FACE_OUTER_BOUND ( 'NONE', #12259, .T. ) ;
#6507=B_SPLINE_CURVE_WITH_KNOTS ( 'NONE', 3,
 ( #1304, #216, #13696, #4688 ),
 .UNSPECIFIED., .F., .F.,
 ( 4, 4 ),
 ( 2.380737581660915015E-07, 0.002336974151641525201 ),
 .UNSPECIFIED. ) ;
#6512=CARTESIAN_POINT ( 'NONE',  ( 6.800000000000084199, 4.618802153517023612, -1.387778780781445676E-14 ) ) ;
#6524=DIRECTION ( 'NONE',  ( 0.000000000000000000, 0.000000000000000000, 1.000000000000000000 ) ) ;
#6536=LINE ( 'NONE', #910, #12178 ) ;
#6571=CARTESIAN_POINT ( 'NONE',  ( 5.103531824934226080, -2.354098498486466351, -4.077418205400154427 ) ) ;
#6574=DIRECTION ( 'NONE',  ( 1.734723475976770502E-18, -4.440892098500621231E-16, -1.000000000000000000 ) ) ;
#6600=CARTESIAN_POINT ( 'NONE',  ( 5.024612689793094944, 2.312654742478284398, 4.005635514337482661 ) ) ;
#6635=DIRECTION ( 'NONE',  ( 0.000000000000000000, -4.440892098500620245E-16, -1.000000000000000000 ) ) ;
#6644=ORIENTED_EDGE ( 'NONE', *, *, #4515, .F. ) ;
#6650=DIRECTION ( 'NONE',  ( -0.7071067811865513475, 3.141989118817382096E-16, 0.7071067811865437980 ) ) ;
#6671=CARTESIAN_POINT ( 'NONE',  ( 5.005339938400140909, 2.401215914016161967, 4.000000000000002665 ) ) ;
#6675=B_SPLINE_CURVE_WITH_KNOTS ( 'NONE', 3,
 ( #3938, #11679, #416, #2766, #346, #6030 ),
 .UNSPECIFIED., .F., .F.,
 ( 4, 2, 4 ),
 ( 0.002336974151641525201, 0.003500975885716433710, 0.004664977619791342220 ),
 .UNSPECIFIED. ) ;
#6679=CARTESIAN_POINT ( 'NONE',  ( 0.2494252716035087192, 1.935831255942378926, 4.000000000000003553 ) ) ;
#6761=CONICAL_SURFACE ( 'NONE', #9809, 4.000000000000004441, 1.047197551196600296 ) ;
#6764=CONICAL_SURFACE ( 'NONE', #10516, 4.000000000000004441, 1.047197551196600296 ) ;
#6771=CARTESIAN_POINT ( 'NONE',  ( 0.1578711657484770381, -1.548887424832829707, -4.000000000000002665 ) ) ;
#6782=CARTESIAN_POINT ( 'NONE',  ( 5.067058822021065723, -4.651083900313782493, -1.401471914501746383E-14 ) ) ;
#6814=CARTESIAN_POINT ( 'NONE',  ( 4.859329672868200944, -2.661112198169292231, 3.390818468129448870 ) ) ;
#6822=CARTESIAN_POINT ( 'NONE',  ( 5.108576227836145733, -2.381533865848265208, 4.077513078102846578 ) ) ;
#6838=CARTESIAN_POINT ( 'NONE',  ( 5.103531824934171013, 4.708196996972911386, -1.387778780781445676E-14 ) ) ;
#6848=TOROIDAL_SURFACE ( 'NONE', #11292, 6.250000000000000000, 0.5499999999999992673 ) ;
#6854=DIRECTION ( 'NONE',  ( 0.000000000000000000, 4.440892098500621231E-16, 1.000000000000000000 ) ) ;
#6857=PLANE ( 'NONE',  #14455 ) ;
#6861=CARTESIAN_POINT ( 'NONE',  ( 0.1586754815284894260, 2.687817229851479972, -3.344563996438210118 ) ) ;
#6862=CARTESIAN_POINT ( 'NONE',  ( 5.000882498481283633, -4.618802153517009401, -2.416538104178194415E-20 ) ) ;
#6887=CARTESIAN_POINT ( 'NONE',  ( 5.013196232911383277, 2.310564645009324014, -4.002015359328510158 ) ) ;
#6889=CARTESIAN_POINT ( 'NONE',  ( 0.1597025669806160231, 1.557591170363314959, 4.000000000000003553 ) ) ;
#6922=ADVANCED_FACE ( 'NONE', ( #9952 ), #9310, .T. ) ;
#6955=CARTESIAN_POINT ( 'NONE',  ( 5.103531824934115946, 2.354098498486452584, 4.077418205400126894 ) ) ;
#6963=FACE_OUTER_BOUND ( 'NONE', #9783, .T. ) ;
#6973=CARTESIAN_POINT ( 'NONE',  ( 4.769962962079064894, -3.046916606660486693, -2.722585630838685766 ) ) ;
#6978=CARTESIAN_POINT ( 'NONE',  ( 0.03363697881254360672, -0.7786124121997077818, -4.000000000000004441 ) ) ;
#6994=VERTEX_POINT ( 'NONE', #12120 ) ;
#6995=( BOUNDED_SURFACE ( )  B_SPLINE_SURFACE ( 3, 2, ( 
 ( #1493, #5935, #8578 ),
 ( #3046, #14162, #9750 ),
 ( #4144, #14303, #3115 ),
 ( #11890, #13209, #12997 ),
 ( #12098, #12921, #13067 ),
 ( #8727, #8515, #9691 ) ),
 .UNSPECIFIED., .F., .F., .F. ) 
 B_SPLINE_SURFACE_WITH_KNOTS ( ( 4, 2, 4 ),
 ( 3, 3 ),
 ( 0.01886329300151613764, 0.02121559706996257316, 0.02356790113840900522 ),
 ( 0.000000000000000000, 1.000000000000000000 ),
 .UNSPECIFIED. ) 
 GEOMETRIC_REPRESENTATION_ITEM ( )  RATIONAL_B_SPLINE_SURFACE ( (
 ( 1.000000000000000000, 0.8047780979744990626, 1.000000000000000000),
 ( 1.000000000000000000, 0.8123789428413605851, 1.000000000000000000),
 ( 1.000000000000000000, 0.8190677778298707246, 1.000000000000000000),
 ( 1.000000000000000000, 0.8192346266087571216, 1.000000000000000000),
 ( 1.000000000000000000, 0.8126126851684565278, 1.000000000000000000),
 ( 1.000000000000000000, 0.8047712636103355743, 1.000000000000000000) ) ) 
 REPRESENTATION_ITEM ( '' )  SURFACE ( )  );
#7009=CARTESIAN_POINT ( 'NONE',  ( 31.80000000000005045, 6.938893903907228378E-15, 2.775557561562891351E-14 ) ) ;
#7010=ORIENTED_EDGE ( 'NONE', *, *, #2494, .F. ) ;
#7047=CARTESIAN_POINT ( 'NONE',  ( 4.942464816488298496, -2.653516201069525238, -3.403975121040109020 ) ) ;
#7048=FACE_OUTER_BOUND ( 'NONE', #5698, .T. ) ;
#7085=EDGE_CURVE ( 'NONE', #568, #8261, #9441, .T. ) ;
#7098=DIRECTION ( 'NONE',  ( -1.734723475976586383E-18, -0.4999999999999990008, 0.8660254037844391517 ) ) ;
#7099=EDGE_CURVE ( 'NONE', #7193, #9446, #3227, .T. ) ;
#7120=CARTESIAN_POINT ( 'NONE',  ( 4.966167347451191816, -2.723760149935152253, -3.431994069539848535 ) ) ;
#7147=CARTESIAN_POINT ( 'NONE',  ( 5.098157279263968000, -2.347014727359302722, -4.065148753898760958 ) ) ;
#7193=VERTEX_POINT ( 'NONE', #401 ) ;
#7213=CARTESIAN_POINT ( 'NONE',  ( 5.551115123125782702E-14, -3.464101615137743728, 2.000000000000001776 ) ) ;
#7253=CARTESIAN_POINT ( 'NONE',  ( 5.551115123125782702E-14, 1.387778780781445676E-14, -4.000000000000003553 ) ) ;
#7267=ORIENTED_EDGE ( 'NONE', *, *, #7085, .F. ) ;
#7281=LINE ( 'NONE', #9407, #5684 ) ;
#7284=ORIENTED_EDGE ( 'NONE', *, *, #12458, .T. ) ;
#7313=DIRECTION ( 'NONE',  ( 1.987661601597216239E-18, 4.440892098500621724E-16, 1.000000000000000000 ) ) ;
#7335=CARTESIAN_POINT ( 'NONE',  ( 0.2486750293982121773, -1.933232340707288888, 4.000000000000003553 ) ) ;
#7340=CARTESIAN_POINT ( 'NONE',  ( 4.962664318264807584, 2.733102959025825562, -3.415681285064340766 ) ) ;
#7354=ORIENTED_EDGE ( 'NONE', *, *, #6151, .T. ) ;
#7415=EDGE_LOOP ( 'NONE', ( #4026, #13852, #2798, #836, #4551, #11823, #8359 ) ) ;
#7422=EDGE_CURVE ( 'NONE', #2703, #10163, #5076, .T. ) ;
#7480=EDGE_CURVE ( 'NONE', #1777, #8457, #5118, .T. ) ;
#7481=VERTEX_POINT ( 'NONE', #12254 ) ;
#7501=B_SPLINE_CURVE_WITH_KNOTS ( 'NONE', 3,
 ( #13366, #5515, #10186, #111 ),
 .UNSPECIFIED., .F., .F.,
 ( 4, 4 ),
 ( 2.380737581874191823E-07, 0.002336974151641544283 ),
 .UNSPECIFIED. ) ;
#7516=B_SPLINE_CURVE_WITH_KNOTS ( 'NONE', 3,
 ( #1287, #2463, #6978, #6771, #3643, #8971 ),
 .UNSPECIFIED., .F., .F.,
 ( 4, 2, 4 ),
 ( 0.01471339550817208665, 0.01588188803962661128, 0.01705038057108113764 ),
 .UNSPECIFIED. ) ;
#7551=ORIENTED_EDGE ( 'NONE', *, *, #1343, .F. ) ;
#7654=CARTESIAN_POINT ( 'NONE',  ( 5.091953023115924459, -4.682427078960499145, -1.387922423807041543E-14 ) ) ;
#7655=VERTEX_POINT ( 'NONE', #12390 ) ;
#7661=ADVANCED_FACE ( 'NONE', ( #2499 ), #10930, .T. ) ;
#7663=B_SPLINE_CURVE_WITH_KNOTS ( 'NONE', 3,
 ( #9969, #8790, #4355, #13272, #3248 ),
 .UNSPECIFIED., .F., .F.,
 ( 4, 1, 4 ),
 ( 0.000000000000000000, 0.002309401076758503622, 0.004618802153517006376 ),
 .UNSPECIFIED. ) ;
#7666=DIRECTION ( 'NONE',  ( 1.000000000000000000, -2.551526159633733968E-19, -1.987661601597216239E-18 ) ) ;
#7670=CARTESIAN_POINT ( 'NONE',  ( 5.108576461337686503, 4.721997478884313537, 0.02371338167649103892 ) ) ;
#7674=AXIS2_PLACEMENT_3D ( 'NONE', #7719, #3356, #12338 ) ;
#7677=CARTESIAN_POINT ( 'NONE',  ( 0.3572655899081733644, 2.309401076758511806, 3.999999999999989786 ) ) ;
#7719=CARTESIAN_POINT ( 'NONE',  ( 6.800000000000028244, -6.938893903907228378E-15, 0.000000000000000000 ) ) ;
#7749=DIRECTION ( 'NONE',  ( 1.734723475976770502E-18, -4.440892098500621231E-16, -1.000000000000000000 ) ) ;
#7756=ADVANCED_FACE ( 'NONE', ( #8341 ), #12987, .F. ) ;
#7761=PRODUCT_DEFINITION ( 'UNKNOWN', '', #5236, #885 ) ;
#7766=CARTESIAN_POINT ( 'NONE',  ( 6.800000000000028244, -6.938893903907228378E-15, 0.000000000000000000 ) ) ;
#7771=CARTESIAN_POINT ( 'NONE',  ( 4.873329151231311052, -3.940175375302611638, 1.320232820537113216 ) ) ;
#7777=DIRECTION ( 'NONE',  ( -1.000000000000000000, 2.551526159633733968E-19, 1.987661601597216239E-18 ) ) ;
#7790=( NAMED_UNIT ( * ) SI_UNIT ( $, .STERADIAN. ) SOLID_ANGLE_UNIT ( ) );
#7798=ORIENTED_EDGE ( 'NONE', *, *, #2702, .F. ) ;
#7825=CARTESIAN_POINT ( 'NONE',  ( 0.000000000000000000, 0.000000000000000000, 0.000000000000000000 ) ) ;
#7833=DIRECTION ( 'NONE',  ( -1.000000000000000000, 2.551526159633733968E-19, 1.987661601597216239E-18 ) ) ;
#7841=CARTESIAN_POINT ( 'NONE',  ( 4.767545695837832831, 0.8009384484996263653, 4.000000000000002665 ) ) ;
#7861=CARTESIAN_POINT ( 'NONE',  ( 4.960471971868402719, 2.742478347466589028, -3.399327657648797629 ) ) ;
#7873=DIRECTION ( 'NONE',  ( 0.000000000000000000, -4.440892098500618766E-16, -1.000000000000000000 ) ) ;
#7886=ORIENTED_EDGE ( 'NONE', *, *, #479, .F. ) ;
#7897=DIRECTION ( 'NONE',  ( 2.168404344970904483E-18, 0.8660254037844375974, -0.5000000000000018874 ) ) ;
#7919=CARTESIAN_POINT ( 'NONE',  ( 0.03458865240850615697, 0.7871057074736870218, 4.000000000000004441 ) ) ;
#7927=CARTESIAN_POINT ( 'NONE',  ( 4.960798468789919369, 2.741591971433226860, 3.400875223032386430 ) ) ;
#7941=( BOUNDED_SURFACE ( )  B_SPLINE_SURFACE ( 3, 2, ( 
 ( #9007, #8185, #6822 ),
 ( #4439, #104, #1263 ),
 ( #8940, #5642, #2227 ),
 ( #7841, #5572, #5908 ),
 ( #2155, #9975, #5979 ),
 ( #6671, #4577, #8864 ) ),
 .UNSPECIFIED., .F., .F., .T. ) 
 B_SPLINE_SURFACE_WITH_KNOTS ( ( 4, 2, 4 ),
 ( 3, 3 ),
 ( 0.01885737098614312032, 0.02120948332636020395, 0.02356159566657728757 ),
 ( 0.000000000000000000, 1.000000000000000000 ),
 .UNSPECIFIED. ) 
 GEOMETRIC_REPRESENTATION_ITEM ( )  RATIONAL_B_SPLINE_SURFACE ( (
 ( 1.000000000000000000, 0.8047781227178442132, 1.000000000000000000),
 ( 1.000000000000000000, 0.8123782226682895180, 1.000000000000000000),
 ( 1.000000000000000000, 0.8190665306020614711, 1.000000000000000000),
 ( 1.000000000000000000, 0.8192358237219363737, 1.000000000000000000),
 ( 1.000000000000000000, 0.8126132530317291547, 1.000000000000000000),
 ( 1.000000000000000000, 0.8047712439471748080, 1.000000000000000000) ) ) 
 REPRESENTATION_ITEM ( '' )  SURFACE ( )  );
#7950=CARTESIAN_POINT ( 'NONE',  ( 6.800000000000028244, -2.309401076758490934, 3.999999999999976019 ) ) ;
#7957=AXIS2_PLACEMENT_3D ( 'NONE', #10312, #9206, #13768 ) ;
#7983=VERTEX_POINT ( 'NONE', #7677 ) ;
#7992=CARTESIAN_POINT ( 'NONE',  ( 4.988724804725841011, 2.309401076758504701, -4.000000000000003553 ) ) ;
#8023=CARTESIAN_POINT ( 'NONE',  ( 1.730488311240535001E-15, 3.268109542640663889, -2.339468227445696158 ) ) ;
#8029=ORIENTED_EDGE ( 'NONE', *, *, #5814, .F. ) ;
#8042=ORIENTED_EDGE ( 'NONE', *, *, #13859, .F. ) ;
#8045=CARTESIAN_POINT ( 'NONE',  ( 5.085139881807298146, -2.270820054029154988, 4.066824291575158234 ) ) ;
#8070=CARTESIAN_POINT ( 'NONE',  ( 5.085009042717535621, -2.271170964606957554, -4.066216496625539634 ) ) ;
#8088=AXIS2_PLACEMENT_3D ( 'NONE', #5433, #12166, #9901 ) ;
#8122=CARTESIAN_POINT ( 'NONE',  ( 5.098157279263967112, 2.347014727359150843, -4.065148753898843559 ) ) ;
#8130=CARTESIAN_POINT ( 'NONE',  ( 4.871660775260041376, -3.136983646853262808, 2.711317785102830502 ) ) ;
#8141=CARTESIAN_POINT ( 'NONE',  ( 4.686019787951550164, -3.464101615137729517, 2.000000000000000444 ) ) ;
#8157=CARTESIAN_POINT ( 'NONE',  ( 4.872112557124452792, 0.7838640816431967639, 4.072377784234222808 ) ) ;
#8183=DIRECTION ( 'NONE',  ( 1.734723475976770502E-18, -4.440892098500621231E-16, -1.000000000000000000 ) ) ;
#8185=CARTESIAN_POINT ( 'NONE',  ( 5.085008806763689826, -2.385860035267069357, 4.000000000000003553 ) ) ;
#8202=CARTESIAN_POINT ( 'NONE',  ( 5.024612689793150899, 2.312654742478270631, -4.005635514337496872 ) ) ;
#8209=FACE_OUTER_BOUND ( 'NONE', #1970, .T. ) ;
#8211=SURFACE_STYLE_FILL_AREA ( #13797 ) ;
#8228=VERTEX_POINT ( 'NONE', #655 ) ;
#8244=CIRCLE ( 'NONE', #1964, 3.000000000000003553 ) ;
#8258=DIRECTION ( 'NONE',  ( -1.734723475976770694E-18, 4.440892098500621231E-16, 1.000000000000000000 ) ) ;
#8261=VERTEX_POINT ( 'NONE', #2026 ) ;
#8268=ORIENTED_EDGE ( 'NONE', *, *, #3496, .T. ) ;
#8272=CLOSED_SHELL ( 'NONE', ( #12286, #5120, #2099, #14416, #1454, #3404, #6321, #12139, #9075, #14005, #4764, #11165, #7661, #6922, #4478, #1960, #5278, #6115, #7756, #3106, #12698, #10882, #9234, #4170, #8416, #10069, #5150, #13635, #2989 ) ) ;
#8280=ORIENTED_EDGE ( 'NONE', *, *, #1445, .T. ) ;
#8282=DIRECTION ( 'NONE',  ( 1.734723475976770502E-18, -4.440892098500621231E-16, -1.000000000000000000 ) ) ;
#8294=CARTESIAN_POINT ( 'NONE',  ( 5.103279350327411201, 4.707503328691851507, -2.309077599722808952E-14 ) ) ;
#8310=EDGE_CURVE ( 'NONE', #10136, #47, #2783, .T. ) ;
#8314=VERTEX_POINT ( 'NONE', #11018 ) ;
#8341=FACE_OUTER_BOUND ( 'NONE', #12735, .T. ) ;
#8359=ORIENTED_EDGE ( 'NONE', *, *, #11603, .T. ) ;
#8371=CARTESIAN_POINT ( 'NONE',  ( 4.844561581013658191, 3.861881939214527826, 1.311024268447660290 ) ) ;
#8390=VERTEX_POINT ( 'NONE', #13883 ) ;
#8398=CARTESIAN_POINT ( 'NONE',  ( 31.80000000000005045, 6.938893903907228378E-15, 2.775557561562891351E-14 ) ) ;
#8400=CARTESIAN_POINT ( 'NONE',  ( 5.013196232911404593, -2.310564645009324902, -4.002015359328471966 ) ) ;
#8412=AXIS2_PLACEMENT_3D ( 'NONE', #2849, #12952, #9712 ) ;
#8416=ADVANCED_FACE ( 'NONE', ( #404 ), #388, .F. ) ;
#8437=( NAMED_UNIT ( * ) SI_UNIT ( $, .STERADIAN. ) SOLID_ANGLE_UNIT ( ) );
#8457=VERTEX_POINT ( 'NONE', #4938 ) ;
#8472=MECHANICAL_DESIGN_GEOMETRIC_PRESENTATION_REPRESENTATION('',(#5879),#10337);
#8503=VERTEX_POINT ( 'NONE', #14239 ) ;
#8515=CARTESIAN_POINT ( 'NONE',  ( 5.085139694532330168, -2.386562117782604631, -4.000000000000001776 ) ) ;
#8526=CARTESIAN_POINT ( 'NONE',  ( 4.988724804725896966, -2.309401076758484272, 4.000000000000003553 ) ) ;
#8543=ORIENTED_EDGE ( 'NONE', *, *, #12426, .F. ) ;
#8553=CARTESIAN_POINT ( 'NONE',  ( 5.091953023115924459, -2.341213539480245576, -4.055100801747961725 ) ) ;
#8559=CARTESIAN_POINT ( 'NONE',  ( -5.551115123125782702E-14, -3.464101615137743728, -2.000000000000015543 ) ) ;
#8578=CARTESIAN_POINT ( 'NONE',  ( 5.108576695057072570, 2.381536396098283159, -4.077513086864523295 ) ) ;
#8584=VERTEX_POINT ( 'NONE', #638 ) ;
#8611=ORIENTED_EDGE ( 'NONE', *, *, #8310, .F. ) ;
#8624=CARTESIAN_POINT ( 'NONE',  ( 5.733169058567799681, -6.938893903907228378E-15, 0.000000000000000000 ) ) ;
#8637=DIRECTION ( 'NONE',  ( -1.000000000000000000, 2.551526159633733968E-19, 1.987661601597216239E-18 ) ) ;
#8649=EDGE_CURVE ( 'NONE', #10570, #10136, #3002, .T. ) ;
#8706=VERTEX_POINT ( 'NONE', #4367 ) ;
#8710=CARTESIAN_POINT ( 'NONE',  ( 0.000000000000000000, 0.000000000000000000, 0.000000000000000000 ) ) ;
#8712=CARTESIAN_POINT ( 'NONE',  ( 0.1586754815284918407, 4.240386000424043011, 0.6554360035617904368 ) ) ;
#8725=DIRECTION ( 'NONE',  ( -1.734723475976770694E-18, 4.440892098500620738E-16, 1.000000000000000000 ) ) ;
#8727=CARTESIAN_POINT ( 'NONE',  ( 5.005339567054419625, -2.401213891501550624, -4.000000000000001776 ) ) ;
#8746=DIRECTION ( 'NONE',  ( -1.000000000000000000, 2.551526159633733968E-19, 1.987661601597216239E-18 ) ) ;
#8750=FILL_AREA_STYLE_COLOUR ( '', #2352 ) ;
#8767=CARTESIAN_POINT ( 'NONE',  ( 5.103531824934171013, -4.708196996972898063, 1.387778780781445676E-14 ) ) ;
#8779=CARTESIAN_POINT ( 'NONE',  ( 0.3572655899082288755, 4.618802153517023612, 1.387778780781445676E-14 ) ) ;
#8780=DIRECTION ( 'NONE',  ( 1.000000000000000000, -2.551526159633733968E-19, -1.987661601597216239E-18 ) ) ;
#8784=EDGE_CURVE ( 'NONE', #7655, #13637, #9984, .T. ) ;
#8789=PLANE ( 'NONE',  #13820 ) ;
#8790=CARTESIAN_POINT ( 'NONE',  ( 4.851472949720940342, -2.694301256218261109, -3.333333333333325932 ) ) ;
#8791=CARTESIAN_POINT ( 'NONE',  ( 4.767554269344977058, -3.063547535897971574, 2.693780016422239854 ) ) ;
#8793=EDGE_CURVE ( 'NONE', #6994, #8314, #14196, .T. ) ;
#8796=B_SPLINE_CURVE_WITH_KNOTS ( 'NONE', 3,
 ( #3407, #11138, #10043, #6600, #13357, #3470, #13435, #14446, #12649, #2290, #2639, #12251, #11209, #12388, #2363, #4897 ),
 .UNSPECIFIED., .F., .F.,
 ( 4, 3, 3, 3, 3, 4 ),
 ( 0.000000000000000000, 3.647308126642597652E-05, 7.269606878412227468E-05, 0.0001129253843484859200, 0.0001515766232005100775, 0.0001537911822990420917 ),
 .UNSPECIFIED. ) ;
#8802=SHAPE_REPRESENTATION ( 'hex flange bolt small_iso_ISO 4162 - M6 x 25 x 25-C', ( #11025 ), #1942 ) ;
#8824=DIRECTION ( 'NONE',  ( 0.000000000000000000, -4.440892098500619752E-16, -1.000000000000000000 ) ) ;
#8829=DIRECTION ( 'NONE',  ( 0.000000000000000000, 4.440892098500620738E-16, 1.000000000000000000 ) ) ;
#8849=CARTESIAN_POINT ( 'NONE',  ( 4.870920456765259310, 3.129869081975187761, -2.723603336645452622 ) ) ;
#8864=CARTESIAN_POINT ( 'NONE',  ( 5.108706126686590743, 2.382237260725047712, 4.077515513881460052 ) ) ;
#8915=CARTESIAN_POINT ( 'NONE',  ( 4.872112557122744825, -2.415761400130177830E-11, -4.072377784234180176 ) ) ;
#8932=DIRECTION ( 'NONE',  ( 0.000000000000000000, 4.440892098500620738E-16, 1.000000000000000000 ) ) ;
#8940=CARTESIAN_POINT ( 'NONE',  ( 4.769971895851991661, -0.8344440309347370688, 4.000000000000002665 ) ) ;
#8960=( NAMED_UNIT ( * ) PLANE_ANGLE_UNIT ( ) SI_UNIT ( $, .RADIAN. ) );
#8971=CARTESIAN_POINT ( 'NONE',  ( 0.3572655899080068309, -2.309401076758678339, -4.000000000000031086 ) ) ;
#8986=ORIENTED_EDGE ( 'NONE', *, *, #13361, .F. ) ;
#9007=CARTESIAN_POINT ( 'NONE',  ( 5.005210039549695900, -2.400508349366352157, 4.000000000000003553 ) ) ;
#9032=CIRCLE ( 'NONE', #4622, 0.5499999999999992673 ) ;
#9047=CONICAL_SURFACE ( 'NONE', #3691, 6.438111078829122036, 1.221730476396037712 ) ;
#9061=EDGE_LOOP ( 'NONE', ( #5061, #7354, #10202, #11891, #11349, #4768, #13320 ) ) ;
#9068=CARTESIAN_POINT ( 'NONE',  ( 0.3572655899081733644, -4.618802153516988973, -1.387778780781445676E-14 ) ) ;
#9072=CARTESIAN_POINT ( 'NONE',  ( 4.988724804725841011, 2.309401076758504701, -4.000000000000003553 ) ) ;
#9075=ADVANCED_FACE ( 'NONE', ( #12133 ), #9047, .T. ) ;
#9105=CARTESIAN_POINT ( 'NONE',  ( 5.103531824934226080, -2.354098498486466351, -4.077418205400154427 ) ) ;
#9112=B_SPLINE_CURVE_WITH_KNOTS ( 'NONE', 3,
 ( #8767, #3221, #12287, #13403, #12359, #7654, #3375, #13536, #6782, #2404, #14414, #1157, #11255, #10083, #6862, #12137 ),
 .UNSPECIFIED., .F., .F.,
 ( 4, 3, 3, 3, 3, 4 ),
 ( -2.214559098546004647E-06, 0.000000000000000000, 3.881464059292318041E-05, 7.921402936568111498E-05, 0.0001155901529638586709, 0.0001522174276056075621 ),
 .UNSPECIFIED. ) ;
#9163=PLANE ( 'NONE',  #2343 ) ;
#9168=CIRCLE ( 'NONE', #3352, 3.000000000000003553 ) ;
#9194=CARTESIAN_POINT ( 'NONE',  ( 0.03421028094653593560, 3.072372537026365702, -2.678494666091054022 ) ) ;
#9206=DIRECTION ( 'NONE',  ( 5.493715166364590271E-32, -0.8660254037844383745, -0.5000000000000005551 ) ) ;
#9234=ADVANCED_FACE ( 'NONE', ( #13747 ), #6857, .F. ) ;
#9250=CARTESIAN_POINT ( 'NONE',  ( 4.939003118777103296, -4.265486753575247647, -0.6119602237977784798 ) ) ;
#9283=DIRECTION ( 'NONE',  ( 1.734723475976770502E-18, -4.440892098500621231E-16, -1.000000000000000000 ) ) ;
#9310=CONICAL_SURFACE ( 'NONE', #11182, 4.000000000000004441, 1.047197551196600296 ) ;
#9314=CARTESIAN_POINT ( 'NONE',  ( 5.733169058567799681, -6.938893903907228378E-15, 0.000000000000000000 ) ) ;
#9315=FILL_AREA_STYLE_COLOUR ( '', #11991 ) ;
#9324=CARTESIAN_POINT ( 'NONE',  ( 4.870920456765268192, -3.923644220354688184, -1.348744467187204199 ) ) ;
#9329=CARTESIAN_POINT ( 'NONE',  ( 5.084394237955924822, 4.671926501058326409, -1.387778780781445676E-14 ) ) ;
#9349=EDGE_LOOP ( 'NONE', ( #10748, #2202, #3282, #11242 ) ) ;
#9351=DIRECTION ( 'NONE',  ( 1.000000000000000000, -2.551526159633733968E-19, -1.987661601597216239E-18 ) ) ;
#9356=CIRCLE ( 'NONE', #8412, 6.438111078829122036 ) ;
#9364=CARTESIAN_POINT ( 'NONE',  ( 31.80000000000005045, 6.152361115950385938E-15, -2.445499999999975138 ) ) ;
#9368=ORIENTED_EDGE ( 'NONE', *, *, #465, .F. ) ;
#9374=EDGE_LOOP ( 'NONE', ( #7798, #3498, #398, #14403, #8042 ) ) ;
#9402=CARTESIAN_POINT ( 'NONE',  ( 4.859329672867496619, 4.267091032106366200, 0.6091815318702697990 ) ) ;
#9407=CARTESIAN_POINT ( 'NONE',  ( -5.204170427930318053E-18, 1.332267629550187849E-15, 3.000000000000003553 ) ) ;
#9438=CARTESIAN_POINT ( 'NONE',  ( 0.000000000000000000, 0.000000000000000000, 0.000000000000000000 ) ) ;
#9441=B_SPLINE_CURVE_WITH_KNOTS ( 'NONE', 3,
 ( #5524, #7861, #13168, #13300, #2179, #3277 ),
 .UNSPECIFIED., .F., .F.,
 ( 4, 2, 4 ),
 ( 0.000000000000000000, 0.002383230369971169656, 0.004766460739942339313 ),
 .UNSPECIFIED. ) ;
#9446=VERTEX_POINT ( 'NONE', #4166 ) ;
#9455=CARTESIAN_POINT ( 'NONE',  ( 5.046772446839294268, 2.317775331972806274, -4.014504635506718877 ) ) ;
#9478=B_SPLINE_CURVE_WITH_KNOTS ( 'NONE', 3,
 ( #2689, #2763, #1354, #2537 ),
 .UNSPECIFIED., .F., .F.,
 ( 4, 4 ),
 ( 2.380737581434041740E-07, 0.002336974151641588518 ),
 .UNSPECIFIED. ) ;
#9479=CARTESIAN_POINT ( 'NONE',  ( 4.872112557122744825, -2.415761400130177830E-11, -4.072377784234180176 ) ) ;
#9482=CARTESIAN_POINT ( 'NONE',  ( 4.769962962078715840, 3.046916606660529325, 2.722585630838614712 ) ) ;
#9511=CARTESIAN_POINT ( 'NONE',  ( 5.084394237956035845, -2.335963250529156543, -4.046007034530258117 ) ) ;
#9536=CARTESIAN_POINT ( 'NONE',  ( 2.371692252312040555E-15, 0.3911686820596244063, -4.000000000000003553 ) ) ;
#9544=( NAMED_UNIT ( * ) PLANE_ANGLE_UNIT ( ) SI_UNIT ( $, .RADIAN. ) );
#9551=CARTESIAN_POINT ( 'NONE',  ( 6.800000000000028244, -4.618802153517003184, 0.000000000000000000 ) ) ;
#9557=CARTESIAN_POINT ( 'NONE',  ( 4.847001880571993659, 3.049720480807994516, 2.717729178357345177 ) ) ;
#9586=CARTESIAN_POINT ( 'NONE',  ( -5.551115123125782702E-14, -3.464101615137743728, -2.000000000000015543 ) ) ;
#9596=EDGE_CURVE ( 'NONE', #8261, #12769, #11013, .T. ) ;
#9632=CARTESIAN_POINT ( 'NONE',  ( 5.103021810857296892, -2.353405741490973035, 4.076218315086694410 ) ) ;
#9683=UNCERTAINTY_MEASURE_WITH_UNIT (LENGTH_MEASURE( 1.000000000000000082E-05 ), #4317, 'distance_accuracy_value', 'NONE');
#9691=CARTESIAN_POINT ( 'NONE',  ( 5.108705755340869459, -2.382235250128048154, -4.077515506918746979 ) ) ;
#9712=DIRECTION ( 'NONE',  ( 0.000000000000000000, 4.440892098500621231E-16, 1.000000000000000000 ) ) ;
#9719=ORIENTED_EDGE ( 'NONE', *, *, #9807, .T. ) ;
#9729=ORIENTED_EDGE ( 'NONE', *, *, #4246, .T. ) ;
#9735=ORIENTED_EDGE ( 'NONE', *, *, #756, .F. ) ;
#9739=CARTESIAN_POINT ( 'NONE',  ( 5.551115123125782702E-14, 3.464101615137764156, 2.000000000000001776 ) ) ;
#9748=CARTESIAN_POINT ( 'NONE',  ( 0.3572655899081733644, -2.309401076758484272, 4.000000000000031086 ) ) ;
#9750=CARTESIAN_POINT ( 'NONE',  ( 4.966160964381386655, 1.610279710338473391, -4.074842399450050223 ) ) ;
#9769=CARTESIAN_POINT ( 'NONE',  ( 5.103531824934115946, -2.354098498486438373, 4.077418205400141105 ) ) ;
#9783=EDGE_LOOP ( 'NONE', ( #11812, #1869, #11595, #5365, #1526 ) ) ;
#9807=EDGE_CURVE ( 'NONE', #3835, #6304, #244, .T. ) ;
#9809=AXIS2_PLACEMENT_3D ( 'NONE', #14376, #9351, #437 ) ;
#9821=FACE_OUTER_BOUND ( 'NONE', #10619, .T. ) ;
#9836=EDGE_LOOP ( 'NONE', ( #12180, #1561, #10300, #4937 ) ) ;
#9888=CARTESIAN_POINT ( 'NONE',  ( 4.847001880572344490, 3.878482749467366819, -1.282270821642922387 ) ) ;
#9900=CARTESIAN_POINT ( 'NONE',  ( 5.085009042717532957, -4.657032265668552995, -0.06621649662555413596 ) ) ;
#9901=DIRECTION ( 'NONE',  ( 0.000000000000000000, 3.216245299353272708E-16, 1.000000000000000000 ) ) ;
#9902=CARTESIAN_POINT ( 'NONE',  ( 31.80000000000005045, 6.938893903907228378E-15, 2.775557561562891351E-14 ) ) ;
#9952=FACE_OUTER_BOUND ( 'NONE', #13777, .T. ) ;
#9953=CARTESIAN_POINT ( 'NONE',  ( 0.000000000000000000, 0.000000000000000000, 0.000000000000000000 ) ) ;
#9969=CARTESIAN_POINT ( 'NONE',  ( 4.988724804725785944, -2.309401076758511806, -3.999999999999989786 ) ) ;
#9973=( LENGTH_UNIT ( ) NAMED_UNIT ( * ) SI_UNIT ( .MILLI., .METRE. ) );
#9975=CARTESIAN_POINT ( 'NONE',  ( 4.939011777414161308, 1.602816961020108844, 4.000000000000002665 ) ) ;
#9984=B_SPLINE_CURVE_WITH_KNOTS ( 'NONE', 3,
 ( #12560, #3871, #2403, #3586 ),
 .UNSPECIFIED., .F., .F.,
 ( 4, 4 ),
 ( 0.002376763279741535111, 0.004766460739942319363 ),
 .UNSPECIFIED. ) ;
#9998=ORIENTED_EDGE ( 'NONE', *, *, #8784, .F. ) ;
#10027=ORIENTED_EDGE ( 'NONE', *, *, #5814, .T. ) ;
#10033=DIRECTION ( 'NONE',  ( -1.000000000000000000, 2.551526159633733968E-19, 1.987661601597216239E-18 ) ) ;
#10043=CARTESIAN_POINT ( 'NONE',  ( 5.013196232911362848, 2.310564645009344442, 4.002015359328507493 ) ) ;
#10061=EDGE_LOOP ( 'NONE', ( #492, #12040 ) ) ;
#10069=ADVANCED_FACE ( 'NONE', ( #1191 ), #7941, .F. ) ;
#10083=CARTESIAN_POINT ( 'NONE',  ( 5.013196232911366401, -4.621129290018641811, -2.775422584047554243E-14 ) ) ;
#10089=EDGE_CURVE ( 'NONE', #12991, #12769, #8796, .T. ) ;
#10106=ADVANCED_BREP_SHAPE_REPRESENTATION ( '', ( #11661, #11025 ), #1942 ) ;
#10136=VERTEX_POINT ( 'NONE', #9586 ) ;
#10159=CARTESIAN_POINT ( 'NONE',  ( 5.005210273051233116, 2.263846804438351512, 4.078902314160334441 ) ) ;
#10163=VERTEX_POINT ( 'NONE', #805 ) ;
#10175=CARTESIAN_POINT ( 'NONE',  ( 0.1586754815284818487, -4.240386000424023472, -0.6554360035618013169 ) ) ;
#10176=VERTEX_POINT ( 'NONE', #672 ) ;
#10186=CARTESIAN_POINT ( 'NONE',  ( 4.538180240577822737E-16, 3.070647092368435693, 2.681483223904234325 ) ) ;
#10202=ORIENTED_EDGE ( 'NONE', *, *, #2359, .T. ) ;
#10285=ORIENTED_EDGE ( 'NONE', *, *, #10089, .F. ) ;
#10299=VECTOR ( 'NONE', #8746, 1000.000000000000000 ) ;
#10300=ORIENTED_EDGE ( 'NONE', *, *, #2349, .T. ) ;
#10310=DIRECTION ( 'NONE',  ( 1.000000000000000000, -2.551526159633733968E-19, -1.987661601597216239E-18 ) ) ;
#10312=CARTESIAN_POINT ( 'NONE',  ( 6.800000000000084199, 4.618802153517023612, -1.387778780781445676E-14 ) ) ;
#10337=( GEOMETRIC_REPRESENTATION_CONTEXT ( 3 ) GLOBAL_UNCERTAINTY_ASSIGNED_CONTEXT ( ( #1488 ) ) GLOBAL_UNIT_ASSIGNED_CONTEXT ( ( #9973, #4215, #968 ) ) REPRESENTATION_CONTEXT ( 'NONE', 'WORKASPACE' ) );
#10354=CARTESIAN_POINT ( 'NONE',  ( 4.988724804725785944, -4.618802153517009401, 0.000000000000000000 ) ) ;
#10396=ORIENTED_EDGE ( 'NONE', *, *, #13305, .T. ) ;
#10398=CARTESIAN_POINT ( 'NONE',  ( 4.988724804725896966, 4.618802153517016507, 1.387778780781445676E-14 ) ) ;
#10404=DIRECTION ( 'NONE',  ( 1.000000000000000000, -2.551526159633733968E-19, -1.987661601597216239E-18 ) ) ;
#10423=CARTESIAN_POINT ( 'NONE',  ( 4.988724804725896966, 4.618802153517016507, 1.387778780781445676E-14 ) ) ;
#10460=CARTESIAN_POINT ( 'NONE',  ( -5.332495919439446207E-15, -3.660093687634839110, -1.660531772554321384 ) ) ;
#10478=DIRECTION ( 'NONE',  ( -8.673617379884692214E-19, 0.8660254037844392627, 0.4999999999999990563 ) ) ;
#10502=CARTESIAN_POINT ( 'NONE',  ( 4.966167347451144742, 2.723760149934941754, 3.431994069539810344 ) ) ;
#10503=CONICAL_SURFACE ( 'NONE', #2556, 2.445500000000002672, 0.7853981633974423948 ) ;
#10510=CARTESIAN_POINT ( 'NONE',  ( 5.013196232911438344, -2.310564645009316909, 4.002015359328495947 ) ) ;
#10516=AXIS2_PLACEMENT_3D ( 'NONE', #12507, #10310, #9283 ) ;
#10555=CARTESIAN_POINT ( 'NONE',  ( 6.250000000000033751, 6.938893903907228378E-15, -1.387778780781445676E-14 ) ) ;
#10560=CARTESIAN_POINT ( 'NONE',  ( 5.103531824934171013, -4.708196996972898063, 1.387778780781445676E-14 ) ) ;
#10567=CARTESIAN_POINT ( 'NONE',  ( 4.851472949720939454, -1.539600717839007871, -3.999999999999990674 ) ) ;
#10570=VERTEX_POINT ( 'NONE', #7213 ) ;
#10619=EDGE_LOOP ( 'NONE', ( #14218, #1238, #11498, #11443 ) ) ;
#10654=CARTESIAN_POINT ( 'NONE',  ( 4.962664318264674357, 4.324618243609340773, 0.6590959511423351014 ) ) ;
#10663=CARTESIAN_POINT ( 'NONE',  ( 5.103531824934115946, 2.354098498486452584, 4.077418205400126894 ) ) ;
#10710=ORIENTED_EDGE ( 'NONE', *, *, #2702, .T. ) ;
#10724=EDGE_CURVE ( 'NONE', #7481, #4363, #1994, .T. ) ;
#10748=ORIENTED_EDGE ( 'NONE', *, *, #14246, .T. ) ;
#10750=FACE_OUTER_BOUND ( 'NONE', #9349, .T. ) ;
#10752=CARTESIAN_POINT ( 'NONE',  ( 5.103531824934226080, -2.354098498486466351, -4.077418205400154427 ) ) ;
#10792=CARTESIAN_POINT ( 'NONE',  ( 4.988724804725896966, -2.309401076758484272, 4.000000000000003553 ) ) ;
#10805=CARTESIAN_POINT ( 'NONE',  ( 5.103279350327357911, -2.353751664345912875, 4.076817471046950025 ) ) ;
#10806=DIRECTION ( 'NONE',  ( -1.000000000000000000, 2.551526159633733968E-19, 1.987661601597216239E-18 ) ) ;
#10866=EDGE_CURVE ( 'NONE', #10163, #10570, #6507, .T. ) ;
#10876=SURFACE_STYLE_FILL_AREA ( #46 ) ;
#10882=ADVANCED_FACE ( 'NONE', ( #11476 ), #5691, .F. ) ;
#10885=ORIENTED_EDGE ( 'NONE', *, *, #2359, .F. ) ;
#10915=FACE_OUTER_BOUND ( 'NONE', #3841, .T. ) ;
#10930=CONICAL_SURFACE ( 'NONE', #12340, 4.000000000000004441, 1.047197551196600296 ) ;
#10971=CARTESIAN_POINT ( 'NONE',  ( 0.2484800633750049170, 4.430380094434251959, 0.3263565795980906126 ) ) ;
#10972=CARTESIAN_POINT ( 'NONE',  ( 4.767554269344631557, 3.063547535898108798, -2.693780016422034684 ) ) ;
#11007=CARTESIAN_POINT ( 'NONE',  ( 0.3572655899080068309, -2.309401076758678339, -4.000000000000031086 ) ) ;
#11011=ORIENTED_EDGE ( 'NONE', *, *, #11374, .F. ) ;
#11013=B_SPLINE_CURVE_WITH_KNOTS ( 'NONE', 3,
 ( #6838, #11436, #1413, #13448, #7927, #2450 ),
 .UNSPECIFIED., .F., .F.,
 ( 4, 2, 4 ),
 ( 0.000000000000000000, 0.002383230369971169223, 0.004766460739942338445 ),
 .UNSPECIFIED. ) ;
#11018=CARTESIAN_POINT ( 'NONE',  ( 0.3572655899081733644, 2.309401076758504701, -3.999999999999989786 ) ) ;
#11024=EDGE_CURVE ( 'NONE', #2255, #6304, #3406, .T. ) ;
#11025=AXIS2_PLACEMENT_3D ( 'NONE', #167, #6524, #5441 ) ;
#11032=DIRECTION ( 'NONE',  ( 1.000000000000000000, -2.551526159633733968E-19, -1.987661601597216239E-18 ) ) ;
#11040=CARTESIAN_POINT ( 'NONE',  ( 4.988724804725896966, 4.618802153517016507, 1.387778780781445676E-14 ) ) ;
#11054=CARTESIAN_POINT ( 'NONE',  ( 4.769962962079068447, 3.881286623614989661, -1.277414369161378849 ) ) ;
#11063=CIRCLE ( 'NONE', #787, 2.445500000000002672 ) ;
#11082=CARTESIAN_POINT ( 'NONE',  ( 0.000000000000000000, 2.081668171172168513E-14, 4.000000000000003553 ) ) ;
#11108=DIRECTION ( 'NONE',  ( -1.000000000000000000, 2.551526159633733968E-19, 1.987661601597216239E-18 ) ) ;
#11138=CARTESIAN_POINT ( 'NONE',  ( 5.000882498481339589, 2.309401076758504701, 4.000000000000031086 ) ) ;
#11165=ADVANCED_FACE ( 'NONE', ( #1602 ), #34, .T. ) ;
#11182=AXIS2_PLACEMENT_3D ( 'NONE', #1239, #1164, #7749 ) ;
#11188=CARTESIAN_POINT ( 'NONE',  ( 0.03421028094653577600, 3.855830693249152397, 1.321505333908953750 ) ) ;
#11195=B_SPLINE_CURVE_WITH_KNOTS ( 'NONE', 3,
 ( #2875, #1766, #6217, #8559 ),
 .UNSPECIFIED., .F., .F.,
 ( 4, 4 ),
 ( 2.380737582602404047E-07, 0.002336974151641542548 ),
 .UNSPECIFIED. ) ;
#11209=CARTESIAN_POINT ( 'NONE',  ( 5.102759246810695259, 2.353060785250063347, 4.075620833351001338 ) ) ;
#11233=B_SPLINE_CURVE_WITH_KNOTS ( 'NONE', 3,
 ( #10663, #1741, #8157, #4807 ),
 .UNSPECIFIED., .F., .F.,
 ( 4, 4 ),
 ( 0.000000000000000000, 0.002376763279741535111 ),
 .UNSPECIFIED. ) ;
#11240=CARTESIAN_POINT ( 'NONE',  ( 4.960798468790029503, -2.741591971433240627, -3.400875223032410855 ) ) ;
#11242=ORIENTED_EDGE ( 'NONE', *, *, #4438, .F. ) ;
#11255=CARTESIAN_POINT ( 'NONE',  ( 5.024612689793150899, -4.625309484956541262, -2.775557561562891351E-14 ) ) ;
#11260=CIRCLE ( 'NONE', #13848, 3.000000000000003553 ) ;
#11263=ORIENTED_EDGE ( 'NONE', *, *, #571, .F. ) ;
#11269=DIRECTION ( 'NONE',  ( -3.469446951953692767E-18, 0.5000000000000018874, 0.8660254037844375974 ) ) ;
#11273=VERTEX_POINT ( 'NONE', #11703 ) ;
#11275=PRODUCT ( 'hex flange bolt small_iso_ISO 4162 - M6 x 25 x 25-C', 'hex flange bolt small_iso_ISO 4162 - M6 x 25 x 25-C', '', ( #5266 ) ) ;
#11292=AXIS2_PLACEMENT_3D ( 'NONE', #10555, #4844, #5997 ) ;
#11295=DIRECTION ( 'NONE',  ( -1.000000000000000000, 2.551526159633733968E-19, 1.987661601597216239E-18 ) ) ;
#11323=CARTESIAN_POINT ( 'NONE',  ( 0.2484800633750003651, 2.497823135841271913, -3.673643420401906390 ) ) ;
#11331=ORIENTED_EDGE ( 'NONE', *, *, #8793, .F. ) ;
#11339=ORIENTED_EDGE ( 'NONE', *, *, #13810, .F. ) ;
#11347=CARTESIAN_POINT ( 'NONE',  ( 4.686019787951623883, 3.464101615137754386, -1.999999999999987566 ) ) ;
#11349=ORIENTED_EDGE ( 'NONE', *, *, #4614, .T. ) ;
#11360=CARTESIAN_POINT ( 'NONE',  ( 4.960471971868334329, -2.742478347466599686, 3.399327657648741674 ) ) ;
#11374=EDGE_CURVE ( 'NONE', #3835, #8314, #13243, .T. ) ;
#11378=CARTESIAN_POINT ( 'NONE',  ( 5.103531824934171013, -4.708196996972898063, 1.387778780781445676E-14 ) ) ;
#11391=DIRECTION ( 'NONE',  ( 0.000000000000000000, 4.440892098500620738E-16, 1.000000000000000000 ) ) ;
#11426=CONICAL_SURFACE ( 'NONE', #5802, 2.445500000000002672, 0.7853981633974423948 ) ;
#11436=CARTESIAN_POINT ( 'NONE',  ( 4.960471971868381402, 4.315143281044153234, 0.6753920894105047701 ) ) ;
#11443=ORIENTED_EDGE ( 'NONE', *, *, #12526, .F. ) ;
#11444=CARTESIAN_POINT ( 'NONE',  ( 4.873329151231326151, -3.113442849146556668, -2.752175560109257013 ) ) ;
#11451=CARTESIAN_POINT ( 'NONE',  ( 4.872568031907684727, -3.130604888704431321, -2.722411753064914564 ) ) ;
#11476=FACE_OUTER_BOUND ( 'NONE', #9374, .T. ) ;
#11481=VECTOR ( 'NONE', #11108, 1000.000000000000000 ) ;
#11498=ORIENTED_EDGE ( 'NONE', *, *, #4438, .T. ) ;
#11521=CARTESIAN_POINT ( 'NONE',  ( 4.873329151231340362, 3.113442849146619285, 2.752175560109197505 ) ) ;
#11523=ORIENTED_EDGE ( 'NONE', *, *, #4246, .F. ) ;
#11571=CARTESIAN_POINT ( 'NONE',  ( 5.103279350327407649, 2.353751664345936412, -4.076817471046929597 ) ) ;
#11594=ORIENTED_EDGE ( 'NONE', *, *, #13678, .F. ) ;
#11595=ORIENTED_EDGE ( 'NONE', *, *, #12813, .F. ) ;
#11600=CARTESIAN_POINT ( 'NONE',  ( 5.000882498481377780, -2.309401076758483384, 4.000000000000005329 ) ) ;
#11603=EDGE_CURVE ( 'NONE', #11273, #8228, #9356, .T. ) ;
#11623=CARTESIAN_POINT ( 'NONE',  ( 5.076540720129291806, -2.330508241952945259, -4.036558682520535513 ) ) ;
#11630=CARTESIAN_POINT ( 'NONE',  ( 0.03421028094652860813, -3.855830693249136853, -1.321505333908961521 ) ) ;
#11636=CARTESIAN_POINT ( 'NONE',  ( 5.005339752383226148, -2.263494164695139421, 4.079513104112300503 ) ) ;
#11638=AXIS2_PLACEMENT_3D ( 'NONE', #4928, #2590, #8282 ) ;
#11647=CARTESIAN_POINT ( 'NONE',  ( 4.988724804725841011, 2.309401076758504701, -4.000000000000003553 ) ) ;
#11661=MANIFOLD_SOLID_BREP ( 'FlangeHexFillet', #8272 ) ;
#11669=CARTESIAN_POINT ( 'NONE',  ( 4.862831555537598049, 2.651660758729716072, 3.407188841443499872 ) ) ;
#11679=CARTESIAN_POINT ( 'NONE',  ( -7.836748827996783582E-15, -3.268109542640645682, 2.339468227445697046 ) ) ;
#11703=CARTESIAN_POINT ( 'NONE',  ( 5.733169058567799681, -9.797989565831383431E-15, -6.438111078829122036 ) ) ;
#11812=ORIENTED_EDGE ( 'NONE', *, *, #11024, .T. ) ;
#11817=CARTESIAN_POINT ( 'NONE',  ( 5.108705940669683088, 2.340113889544011894, -4.101834868599443240 ) ) ;
#11823=ORIENTED_EDGE ( 'NONE', *, *, #13420, .T. ) ;
#11858=DIRECTION ( 'NONE',  ( -1.000000000000000000, 2.551526159633733968E-19, 1.987661601597216239E-18 ) ) ;
#11890=CARTESIAN_POINT ( 'NONE',  ( 4.767562852629141368, -0.8012780123931543264, -4.000000000000002665 ) ) ;
#11891=ORIENTED_EDGE ( 'NONE', *, *, #13420, .F. ) ;
#11892=B_SPLINE_CURVE_WITH_KNOTS ( 'NONE', 3,
 ( #2816, #4848, #3907, #2509, #9536, #7253 ),
 .UNSPECIFIED., .F., .F.,
 ( 4, 2, 4 ),
 ( 0.01237452868508166076, 0.01354396209662687284, 0.01471339550817208665 ),
 .UNSPECIFIED. ) ;
#11898=CYLINDRICAL_SURFACE ( 'NONE', #5227, 3.000000000000003553 ) ;
#11901=CARTESIAN_POINT ( 'NONE',  ( 4.851472949721053141, 1.539600717839007205, 4.000000000000032863 ) ) ;
#11922=ORIENTED_EDGE ( 'NONE', *, *, #14170, .F. ) ;
#11925=DIRECTION ( 'NONE',  ( -1.000000000000000000, 2.551526159633733968E-19, 1.987661601597216239E-18 ) ) ;
#11955=CARTESIAN_POINT ( 'NONE',  ( 0.1578711657514496047, -1.548887424847043448, 4.000000000000005329 ) ) ;
#11961=SURFACE_STYLE_USAGE ( .BOTH. , #2742 ) ;
#11991=COLOUR_RGB ( '', 0.72549020, 0.75294118, 0.79215686) ;
#12013=CARTESIAN_POINT ( 'NONE',  ( 4.960860176462370319, -1.574785417369796159, -4.074727069546307590 ) ) ;
#12040=ORIENTED_EDGE ( 'NONE', *, *, #465, .T. ) ;
#12042=CARTESIAN_POINT ( 'NONE',  ( 4.988724804725896966, 2.309401076758504701, 4.000000000000031086 ) ) ;
#12063=EDGE_LOOP ( 'NONE', ( #12677, #8268, #1922 ) ) ;
#12082=CARTESIAN_POINT ( 'NONE',  ( 5.005210273051236669, 4.664356425837167919, 0.07890231416034156064 ) ) ;
#12098=CARTESIAN_POINT ( 'NONE',  ( 4.859320940307197745, -1.605931023280709358, -4.000000000000001776 ) ) ;
#12120=CARTESIAN_POINT ( 'NONE',  ( -5.551115123125782702E-14, 3.464101615137750390, -2.000000000000001776 ) ) ;
#12133=FACE_OUTER_BOUND ( 'NONE', #7415, .T. ) ;
#12137=CARTESIAN_POINT ( 'NONE',  ( 4.988724804725785944, -4.618802153517009401, 0.000000000000000000 ) ) ;
#12139=ADVANCED_FACE ( 'NONE', ( #12650 ), #1464, .F. ) ;
#12166=DIRECTION ( 'NONE',  ( 2.551526159633727709E-19, 1.000000000000000000, -3.216245299353268271E-16 ) ) ;
#12173=CARTESIAN_POINT ( 'NONE',  ( 6.800000000000028244, -6.938893903907228378E-15, 0.000000000000000000 ) ) ;
#12178=VECTOR ( 'NONE', #2022, 1000.000000000000000 ) ;
#12180=ORIENTED_EDGE ( 'NONE', *, *, #3386, .F. ) ;
#12200=ORIENTED_EDGE ( 'NONE', *, *, #4804, .T. ) ;
#12244=CARTESIAN_POINT ( 'NONE',  ( 4.844561581013646645, -3.066321291060821963, 2.688975731552646131 ) ) ;
#12251=CARTESIAN_POINT ( 'NONE',  ( 5.098157279264020403, 2.347014727359276520, 4.065148753898767175 ) ) ;
#12254=CARTESIAN_POINT ( 'NONE',  ( 5.551115123125782702E-14, 3.464101615137764156, 2.000000000000001776 ) ) ;
#12259=EDGE_LOOP ( 'NONE', ( #4598, #4010, #10710, #11339, #3618 ) ) ;
#12286=ADVANCED_FACE ( 'NONE', ( #6489 ), #2863, .T. ) ;
#12287=CARTESIAN_POINT ( 'NONE',  ( 5.103021810857247154, -4.706811482981973604, 5.672048699061844739E-14 ) ) ;
#12313=CARTESIAN_POINT ( 'NONE',  ( 5.005210273051227787, -4.664356425837157261, -0.07890231416034962364 ) ) ;
#12324=CARTESIAN_POINT ( 'NONE',  ( 0.3572655899081733644, 2.309401076758511806, 3.999999999999989786 ) ) ;
#12331=AXIS2_PLACEMENT_3D ( 'NONE', #14452, #13218, #3190 ) ;
#12338=DIRECTION ( 'NONE',  ( 0.000000000000000000, -3.108624468950437130E-15, -1.000000000000000000 ) ) ;
#12340=AXIS2_PLACEMENT_3D ( 'NONE', #4706, #10404, #165 ) ;
#12352=DIRECTION ( 'NONE',  ( 3.469446951953791374E-18, -0.5000000000000012212, -0.8660254037844380415 ) ) ;
#12359=CARTESIAN_POINT ( 'NONE',  ( 5.098157279263968000, -4.694029454718629424, -2.227990823963161669E-13 ) ) ;
#12383=CARTESIAN_POINT ( 'NONE',  ( 4.862831555537458605, -4.276542471545712765, 0.5928111585566232522 ) ) ;
#12388=CARTESIAN_POINT ( 'NONE',  ( 5.103021810857296892, 2.353405741490996128, 4.076218315086678423 ) ) ;
#12390=CARTESIAN_POINT ( 'NONE',  ( 4.872112557122744825, 2.415041619695410755E-11, 4.072377784234180176 ) ) ;
#12425=AXIS2_PLACEMENT_3D ( 'NONE', #7009, #2486, #8258 ) ;
#12426=EDGE_CURVE ( 'NONE', #8706, #2703, #9112, .T. ) ;
#12449=VECTOR ( 'NONE', #4980, 1000.000000000000000 ) ;
#12458=EDGE_CURVE ( 'NONE', #8390, #5783, #70, .T. ) ;
#12465=B_SPLINE_CURVE_WITH_KNOTS ( 'NONE', 3,
 ( #10423, #4868, #1427, #5873, #4799, #3710, #640, #13736, #3860, #9329, #5020, #13813, #2685, #5084, #8294, #12768 ),
 .UNSPECIFIED., .F., .F.,
 ( 4, 3, 3, 3, 3, 4 ),
 ( 0.000000000000000000, 3.647308126642503462E-05, 7.269606878412154284E-05, 0.0001129253843484836974, 0.0001515766232005116496, 0.0001537911822990434198 ),
 .UNSPECIFIED. ) ;
#12487=CARTESIAN_POINT ( 'NONE',  ( 4.960471971868395613, -4.315143281044174550, -0.6753920894104464834 ) ) ;
#12506=CARTESIAN_POINT ( 'NONE',  ( 4.960411150172102879, 1.572332708191227058, -4.074718599813436093 ) ) ;
#12507=CARTESIAN_POINT ( 'NONE',  ( 0.000000000000000000, 0.000000000000000000, 0.000000000000000000 ) ) ;
#12526=EDGE_CURVE ( 'NONE', #8584, #6205, #11260, .T. ) ;
#12529=DIRECTION ( 'NONE',  ( -3.469446951953772885E-18, -7.771561172376088880E-16, 1.000000000000000000 ) ) ;
#12560=CARTESIAN_POINT ( 'NONE',  ( 4.872112557122744825, 2.415041619695410755E-11, 4.072377784234180176 ) ) ;
#12585=ORIENTED_EDGE ( 'NONE', *, *, #3027, .F. ) ;
#12649=CARTESIAN_POINT ( 'NONE',  ( 5.076540720129295359, 2.330508241952952808, 4.036558682520539065 ) ) ;
#12650=FACE_OUTER_BOUND ( 'NONE', #4885, .T. ) ;
#12654=DIRECTION ( 'NONE',  ( -0.7071067811865513475, -2.272424659682189540E-16, -0.7071067811865437980 ) ) ;
#12671=VECTOR ( 'NONE', #6650, 1000.000000000000000 ) ;
#12677=ORIENTED_EDGE ( 'NONE', *, *, #10724, .T. ) ;
#12678=CARTESIAN_POINT ( 'NONE',  ( 6.800000000000028244, 2.309401076758504701, -4.000000000000003553 ) ) ;
#12698=ADVANCED_FACE ( 'NONE', ( #6503 ), #1172, .F. ) ;
#12711=DIRECTION ( 'NONE',  ( -1.000000000000000000, 2.551526159633733968E-19, 1.987661601597216239E-18 ) ) ;
#12726=CARTESIAN_POINT ( 'NONE',  ( 5.103021810857252483, -2.353405741491008119, -4.076218315086701516 ) ) ;
#12735=EDGE_LOOP ( 'NONE', ( #4137, #5817, #14274, #4665, #8986 ) ) ;
#12744=CARTESIAN_POINT ( 'NONE',  ( 5.091953023115925347, 2.341213539480247352, -4.055100801747951067 ) ) ;
#12747=B_SPLINE_CURVE_WITH_KNOTS ( 'NONE', 3,
 ( #8526, #1948, #14174, #11901, #12042 ),
 .UNSPECIFIED., .F., .F.,
 ( 4, 1, 4 ),
 ( 0.000000000000000000, 0.002309401076758495382, 0.004618802153516990763 ),
 .UNSPECIFIED. ) ;
#12748=UNCERTAINTY_MEASURE_WITH_UNIT (LENGTH_MEASURE( 1.000000000000000082E-05 ), #1791, 'distance_accuracy_value', 'NONE');
#12766=CARTESIAN_POINT ( 'NONE',  ( 4.859329672867314542, -4.267091032106372417, -0.6091815318702474835 ) ) ;
#12768=CARTESIAN_POINT ( 'NONE',  ( 5.103531824934171013, 4.708196996972911386, -1.387778780781445676E-14 ) ) ;
#12769=VERTEX_POINT ( 'NONE', #6955 ) ;
#12798=CARTESIAN_POINT ( 'NONE',  ( 5.056385618527004411, -2.321455725013326976, -4.020879263244736990 ) ) ;
#12813=EDGE_CURVE ( 'NONE', #568, #3835, #4774, .T. ) ;
#12820=ORIENTED_EDGE ( 'NONE', *, *, #8793, .T. ) ;
#12849=CARTESIAN_POINT ( 'NONE',  ( 4.939003118778239276, 4.265486753573743961, 0.6119602237974551828 ) ) ;
#12879=CARTESIAN_POINT ( 'NONE',  ( 5.000882498481302285, -2.309401076758511806, -3.999999999999989786 ) ) ;
#12900=VECTOR ( 'NONE', #14412, 1000.000000000000000 ) ;
#12921=CARTESIAN_POINT ( 'NONE',  ( 4.938994369585081756, -1.602723107909851619, -4.000000000000001776 ) ) ;
#12923=CARTESIAN_POINT ( 'NONE',  ( 4.966167347451064806, 4.334074124826262420, -0.6428484488893171367 ) ) ;
#12926=B_SPLINE_CURVE_WITH_KNOTS ( 'NONE', 3,
 ( #10354, #3701, #8141, #4151, #10792 ),
 .UNSPECIFIED., .F., .F.,
 ( 4, 1, 4 ),
 ( 0.000000000000000000, 0.002309401076758505356, 0.004618802153517010713 ),
 .UNSPECIFIED. ) ;
#12944=ORIENTED_EDGE ( 'NONE', *, *, #1445, .F. ) ;
#12945=CARTESIAN_POINT ( 'NONE',  ( 5.067058822021064834, -2.325541950156881033, 4.027956812804549536 ) ) ;
#12952=DIRECTION ( 'NONE',  ( -1.000000000000000000, 2.551526159633733968E-19, 1.987661601597216239E-18 ) ) ;
#12979=ORIENTED_EDGE ( 'NONE', *, *, #522, .T. ) ;
#12987=PLANE ( 'NONE',  #13517 ) ;
#12991=VERTEX_POINT ( 'NONE', #1926 ) ;
#12996=LINE ( 'NONE', #627, #14054 ) ;
#12997=CARTESIAN_POINT ( 'NONE',  ( 4.870929040049785108, -0.7939434348317983003, -4.072348019690683607 ) ) ;
#13067=CARTESIAN_POINT ( 'NONE',  ( 4.962655643710850661, -1.591468071165726528, -4.074777072973637893 ) ) ;
#13085=LINE ( 'NONE', #593, #10299 ) ;
#13099=CARTESIAN_POINT ( 'NONE',  ( 6.800000000000028244, -6.938893903907228378E-15, 0.000000000000000000 ) ) ;
#13155=EDGE_CURVE ( 'NONE', #2725, #8584, #4694, .T. ) ;
#13157=EDGE_LOOP ( 'NONE', ( #1627, #4463, #4157 ) ) ;
#13161=CARTESIAN_POINT ( 'NONE',  ( 5.098157279264019515, -2.347014727359296948, 4.065148753898753853 ) ) ;
#13168=CARTESIAN_POINT ( 'NONE',  ( 4.871660775260050258, 3.136983646853265029, -2.711317785102856259 ) ) ;
#13182=SHAPE_DEFINITION_REPRESENTATION ( #171, #8802 ) ;
#13209=CARTESIAN_POINT ( 'NONE',  ( 4.844570275110086754, -0.7957299432388361682, -4.000000000000002665 ) ) ;
#13210=PRESENTATION_STYLE_ASSIGNMENT (( #11961 ) ) ;
#13218=DIRECTION ( 'NONE',  ( 1.000000000000000000, -2.551526159633733968E-19, -1.987661601597216239E-18 ) ) ;
#13221=EDGE_LOOP ( 'NONE', ( #7886, #9729, #1109, #11331, #5695 ) ) ;
#13225=FACE_OUTER_BOUND ( 'NONE', #3078, .T. ) ;
#13243=LINE ( 'NONE', #3218, #12900 ) ;
#13258=DIRECTION ( 'NONE',  ( 3.469446951953772885E-18, 7.771561172376088880E-16, -1.000000000000000000 ) ) ;
#13272=CARTESIAN_POINT ( 'NONE',  ( 4.851472949720941230, -4.233901974057260986, -0.6666666666666652974 ) ) ;
#13273=CARTESIAN_POINT ( 'NONE',  ( 4.939003118777821832, -2.662716476701425083, 3.388039776202045328 ) ) ;
#13300=CARTESIAN_POINT ( 'NONE',  ( 4.872568031907690056, 3.922980182067759891, -1.349977486297356144 ) ) ;
#13305=EDGE_CURVE ( 'NONE', #10136, #10163, #2313, .T. ) ;
#13320=ORIENTED_EDGE ( 'NONE', *, *, #9596, .T. ) ;
#13330=LINE ( 'NONE', #5621, #12671 ) ;
#13340=ORIENTED_EDGE ( 'NONE', *, *, #12426, .T. ) ;
#13350=CARTESIAN_POINT ( 'NONE',  ( 4.942464816486591417, -4.274687029205462174, 0.5960248789590811835 ) ) ;
#13353=CARTESIAN_POINT ( 'NONE',  ( 4.988724804725785944, -2.309401076758511806, -3.999999999999989786 ) ) ;
#13357=CARTESIAN_POINT ( 'NONE',  ( 5.035982117295126237, 2.314736229921496413, 4.009240756344441436 ) ) ;
#13361=EDGE_CURVE ( 'NONE', #5931, #10136, #11195, .T. ) ;
#13366=CARTESIAN_POINT ( 'NONE',  ( 0.3572655899081733644, 2.309401076758511806, 3.999999999999989786 ) ) ;
#13389=CARTESIAN_POINT ( 'NONE',  ( 5.103531824934171013, 2.354098498486459246, -4.077418205400141105 ) ) ;
#13403=CARTESIAN_POINT ( 'NONE',  ( 5.102759246810640192, -4.706121570500099160, 4.163336342344337027E-14 ) ) ;
#13420=EDGE_CURVE ( 'NONE', #14288, #11273, #3966, .T. ) ;
#13435=CARTESIAN_POINT ( 'NONE',  ( 5.056385618527004411, 2.321455725013347848, 4.020879263244750312 ) ) ;
#13448=CARTESIAN_POINT ( 'NONE',  ( 4.872568031907691832, 3.130604888704443756, 2.722411753064904794 ) ) ;
#13480=PLANE ( 'NONE',  #1550 ) ;
#13517=AXIS2_PLACEMENT_3D ( 'NONE', #13928, #10478, #7098 ) ;
#13536=CARTESIAN_POINT ( 'NONE',  ( 5.076540720129292694, -4.661016483905897623, -1.387629536817191694E-14 ) ) ;
#13546=ORIENTED_EDGE ( 'NONE', *, *, #10866, .T. ) ;
#13558=EDGE_CURVE ( 'NONE', #12991, #8503, #14350, .T. ) ;
#13580=DIRECTION ( 'NONE',  ( 8.138903065828892551E-32, -1.000000000000000000, -7.771561172376088880E-16 ) ) ;
#13596=CARTESIAN_POINT ( 'NONE',  ( 5.005339752383235918, -4.664709065580361802, 0.07951310411232598296 ) ) ;
#13627=CARTESIAN_POINT ( 'NONE',  ( 4.872112557121028864, 0.7881298154076051832, -4.072377784234137543 ) ) ;
#13633=VECTOR ( 'NONE', #12654, 1000.000000000000000 ) ;
#13635=ADVANCED_FACE ( 'NONE', ( #7048 ), #5878, .F. ) ;
#13637=VERTEX_POINT ( 'NONE', #1504 ) ;
#13678=EDGE_CURVE ( 'NONE', #8390, #12991, #12747, .T. ) ;
#13684=DIRECTION ( 'NONE',  ( -8.673617379882015172E-19, -0.8660254037844380415, 0.5000000000000012212 ) ) ;
#13696=CARTESIAN_POINT ( 'NONE',  ( -5.922811742559419150E-15, -3.857556137907073524, 1.318516776095761234 ) ) ;
#13706=EDGE_LOOP ( 'NONE', ( #13546, #951, #10396 ) ) ;
#13708=CARTESIAN_POINT ( 'NONE',  ( 5.108705940669676870, -2.340113889543992354, 4.101834868599441464 ) ) ;
#13713=CARTESIAN_POINT ( 'NONE',  ( 5.102759246810640192, 2.353060785250084219, -4.075620833350987127 ) ) ;
#13736=CARTESIAN_POINT ( 'NONE',  ( 5.067058822021044406, 4.651083900313779829, 4.104209016975491201E-18 ) ) ;
#13740=DIRECTION ( 'NONE',  ( -1.000000000000000000, 2.551526159633733968E-19, 1.987661601597216239E-18 ) ) ;
#13747=FACE_OUTER_BOUND ( 'NONE', #13221, .T. ) ;
#13768=DIRECTION ( 'NONE',  ( 8.673617379882821173E-19, 0.5000000000000005551, -0.8660254037844383745 ) ) ;
#13775=CARTESIAN_POINT ( 'NONE',  ( -5.551115123125782702E-14, -3.464101615137743728, -2.000000000000015543 ) ) ;
#13777=EDGE_LOOP ( 'NONE', ( #459, #6449, #1402 ) ) ;
#13778=EDGE_CURVE ( 'NONE', #6205, #8584, #9168, .T. ) ;
#13782=CIRCLE ( 'NONE', #5809, 2.445500000000002672 ) ;
#13786=CARTESIAN_POINT ( 'NONE',  ( 5.103531824934171013, 2.354098498486459246, -4.077418205400141105 ) ) ;
#13797=FILL_AREA_STYLE ('',( #9315 ) ) ;
#13809=CARTESIAN_POINT ( 'NONE',  ( 4.962664318265050056, -4.324618243610393264, -0.6590959511430992679 ) ) ;
#13810=EDGE_CURVE ( 'NONE', #630, #7983, #2812, .T. ) ;
#13813=CARTESIAN_POINT ( 'NONE',  ( 5.098157279264013297, 4.694029454718616989, 9.324225811086985581E-14 ) ) ;
#13820=AXIS2_PLACEMENT_3D ( 'NONE', #6512, #4431, #14037 ) ;
#13848=AXIS2_PLACEMENT_3D ( 'NONE', #5739, #12711, #11391 ) ;
#13852=ORIENTED_EDGE ( 'NONE', *, *, #8784, .T. ) ;
#13859=EDGE_CURVE ( 'NONE', #7983, #7481, #7501, .T. ) ;
#13883=CARTESIAN_POINT ( 'NONE',  ( 4.988724804725896966, -2.309401076758484272, 4.000000000000003553 ) ) ;
#13884=CARTESIAN_POINT ( 'NONE',  ( 5.005339752383242136, 4.664709065580363578, -0.07951310411231406194 ) ) ;
#13886=PRESENTATION_STYLE_ASSIGNMENT (( #3275 ) ) ;
#13914=CARTESIAN_POINT ( 'NONE',  ( 5.024612689793206854, -2.312654742478277736, -4.005635514337468450 ) ) ;
#13928=CARTESIAN_POINT ( 'NONE',  ( 6.799999999999972289, -2.309401076758498039, -4.000000000000003553 ) ) ;
#13959=CARTESIAN_POINT ( 'NONE',  ( 5.102759246810695259, -2.353060785250042475, 4.075620833351015548 ) ) ;
#13991=ORIENTED_EDGE ( 'NONE', *, *, #7422, .F. ) ;
#14003=CARTESIAN_POINT ( 'NONE',  ( 0.000000000000000000, 0.000000000000000000, 0.000000000000000000 ) ) ;
#14005=ADVANCED_FACE ( 'NONE', ( #5929 ), #6848, .T. ) ;
#14029=DIRECTION ( 'NONE',  ( -1.000000000000000000, 2.551526159633733968E-19, 1.987661601597216239E-18 ) ) ;
#14030=DIRECTION ( 'NONE',  ( -1.734723475976770694E-18, 4.440892098500620738E-16, 1.000000000000000000 ) ) ;
#14034=CARTESIAN_POINT ( 'NONE',  ( 4.870920456765266415, 3.923644220354623791, 1.348744467187277474 ) ) ;
#14037=DIRECTION ( 'NONE',  ( 1.734723475976770694E-18, -4.440892098500621231E-16, -1.000000000000000000 ) ) ;
#14043=CARTESIAN_POINT ( 'NONE',  ( 5.084394237956035845, -2.335963250529142332, 4.046007034530258117 ) ) ;
#14054=VECTOR ( 'NONE', #2899, 1000.000000000000000 ) ;
#14162=CARTESIAN_POINT ( 'NONE',  ( 4.942458497589258037, 1.621137229507842781, -4.000000000000002665 ) ) ;
#14170=EDGE_CURVE ( 'NONE', #8457, #1777, #3598, .T. ) ;
#14174=CARTESIAN_POINT ( 'NONE',  ( 4.686019787951567928, 9.324138683375338132E-15, 3.999999999999974243 ) ) ;
#14192=CARTESIAN_POINT ( 'NONE',  ( 6.800000000000084199, 4.618802153517023612, -1.387778780781445676E-14 ) ) ;
#14196=B_SPLINE_CURVE_WITH_KNOTS ( 'NONE', 3,
 ( #5892, #8023, #9194, #6861, #11323, #1443 ),
 .UNSPECIFIED., .F., .F.,
 ( 4, 2, 4 ),
 ( 0.002336974151641588518, 0.003500975885716462767, 0.004664977619791337016 ),
 .UNSPECIFIED. ) ;
#14218=ORIENTED_EDGE ( 'NONE', *, *, #13155, .F. ) ;
#14239=CARTESIAN_POINT ( 'NONE',  ( 4.988724804725896966, 4.618802153517016507, 1.387778780781445676E-14 ) ) ;
#14246=EDGE_CURVE ( 'NONE', #10176, #2725, #11063, .T. ) ;
#14248=CARTESIAN_POINT ( 'NONE',  ( 5.076540720129293582, -2.330508241952930604, 4.036558682520535513 ) ) ;
#14274=ORIENTED_EDGE ( 'NONE', *, *, #7422, .T. ) ;
#14280=STYLED_ITEM ( 'NONE', ( #13886 ), #11661 ) ;
#14288=VERTEX_POINT ( 'NONE', #9479 ) ;
#14299=CARTESIAN_POINT ( 'NONE',  ( 0.000000000000000000, 0.000000000000000000, 0.000000000000000000 ) ) ;
#14303=CARTESIAN_POINT ( 'NONE',  ( 4.846992820204762076, 0.8286880900430499963, -4.000000000000002665 ) ) ;
#14317=EDGE_LOOP ( 'NONE', ( #13340, #7551, #5616, #11263 ) ) ;
#14329=DIRECTION ( 'NONE',  ( 1.734723475976770502E-18, -4.440892098500621231E-16, -1.000000000000000000 ) ) ;
#14350=B_SPLINE_CURVE_WITH_KNOTS ( 'NONE', 3,
 ( #2120, #6495, #3299, #1017, #11040 ),
 .UNSPECIFIED., .F., .F.,
 ( 4, 1, 4 ),
 ( 0.000000000000000000, 0.002309401076758504055, 0.004618802153517008978 ),
 .UNSPECIFIED. ) ;
#14359=CARTESIAN_POINT ( 'NONE',  ( 5.085009042717541838, 4.657032265668563653, 0.06621649662554610072 ) ) ;
#14376=CARTESIAN_POINT ( 'NONE',  ( 0.000000000000000000, 0.000000000000000000, 0.000000000000000000 ) ) ;
#14386=CARTESIAN_POINT ( 'NONE',  ( 31.24550000000003536, 0.000000000000000000, 0.000000000000000000 ) ) ;
#14399=EDGE_CURVE ( 'NONE', #2703, #8390, #12926, .T. ) ;
#14403=ORIENTED_EDGE ( 'NONE', *, *, #10724, .F. ) ;
#14405=ORIENTED_EDGE ( 'NONE', *, *, #1057, .T. ) ;
#14412=DIRECTION ( 'NONE',  ( -1.000000000000000000, 2.551526159633733968E-19, 1.987661601597216239E-18 ) ) ;
#14414=CARTESIAN_POINT ( 'NONE',  ( 5.046772446839293380, -4.635550663945605443, -1.375445609632852674E-14 ) ) ;
#14416=ADVANCED_FACE ( 'NONE', ( #4085 ), #11898, .T. ) ;
#14423=CIRCLE ( 'NONE', #8088, 0.5499999999999992673 ) ;
#14446=CARTESIAN_POINT ( 'NONE',  ( 5.067058822021063058, 2.325541950156907234, 4.027956812804561082 ) ) ;
#14450=DIRECTION ( 'NONE',  ( 0.000000000000000000, 4.440892098500621231E-16, 1.000000000000000000 ) ) ;
#14452=CARTESIAN_POINT ( 'NONE',  ( 0.000000000000000000, 0.000000000000000000, 0.000000000000000000 ) ) ;
#14455=AXIS2_PLACEMENT_3D ( 'NONE', #2544, #13684, #12352 ) ;
ENDSEC;
END-ISO-10303-21;
